ISO-10303-21;
HEADER;
FILE_DESCRIPTION (('STEP AP214'),
    '1' );
FILE_NAME ('Tapered Toolholder Shank.step',
    '2026-10-09T18:50:44',
    ( '' ),
    ( '' ),
    'SwSTEP 2.0',
    'SolidWorks 2026',
    '' );
FILE_SCHEMA (( 'AUTOMOTIVE_DESIGN' ));
ENDSEC;

DATA;
#19=CYLINDRICAL_SURFACE ( 'NONE', #13148, 15.62500000000000000 ) ;
#26=CARTESIAN_POINT ( 'NONE',  ( -19.99969986081099904, -13.50737899243800122, -13.01695671647154917 ) ) ;
#29=ORIENTED_EDGE ( 'NONE', *, *, #1222, .T. ) ;
#39=CARTESIAN_POINT ( 'NONE',  ( -15.49969986081099904, 10.68321993080349763, 24.21206422150099868 ) ) ;
#41=CIRCLE ( 'NONE', #1011, 2.500000000000002220 ) ;
#45=ORIENTED_EDGE ( 'NONE', *, *, #9054, .F. ) ;
#47=CARTESIAN_POINT ( 'NONE',  ( -19.40475874296427250, -15.76281827183478512, -13.08441654828304657 ) ) ;
#50=CYLINDRICAL_SURFACE ( 'NONE', #2747, 15.62500000000000000 ) ;
#59=CARTESIAN_POINT ( 'NONE',  ( -37.04494295528539993, 3.992621007561997892, 24.16206422150099442 ) ) ;
#71=DIRECTION ( 'NONE',  ( 0.000000000000000000, 0.000000000000000000, 1.000000000000000000 ) ) ;
#75=DIRECTION ( 'NONE',  ( 1.000000000000000000, 0.000000000000000000, 0.000000000000000000 ) ) ;
#79=AXIS2_PLACEMENT_3D ( 'NONE', #11806, #5987, #8360 ) ;
#81=CARTESIAN_POINT ( 'NONE',  ( -15.49969986081099904, -32.00737899243799944, 24.21206422150100224 ) ) ;
#88=PLANE ( 'NONE',  #6660 ) ;
#89=EDGE_LOOP ( 'NONE', ( #13517, #1080, #433, #4734 ) ) ;
#90=ORIENTED_EDGE ( 'NONE', *, *, #9916, .T. ) ;
#91=CIRCLE ( 'NONE', #14500, 8.000000000000000000 ) ;
#92=CIRCLE ( 'NONE', #3743, 3.249999999999999556 ) ;
#93=EDGE_CURVE ( 'NONE', #6978, #3447, #6411, .T. ) ;
#106=CARTESIAN_POINT ( 'NONE',  ( -5.499699860810999041, -13.50737899243800122, 6.712064221500998684 ) ) ;
#109=CARTESIAN_POINT ( 'NONE',  ( -14.90757383352018195, -17.97794807782672777, -13.28437183209255146 ) ) ;
#110=ORIENTED_EDGE ( 'NONE', *, *, #5500, .T. ) ;
#120=LINE ( 'NONE', #11886, #1708 ) ;
#122=AXIS2_PLACEMENT_3D ( 'NONE', #7053, #14187, #10744 ) ;
#133=EDGE_LOOP ( 'NONE', ( #10977, #6757, #1819, #5580 ) ) ;
#138=CARTESIAN_POINT ( 'NONE',  ( 7.500245791298697284, 3.992621007561997892, 24.26206422150100295 ) ) ;
#140=ADVANCED_FACE ( 'NONE', ( #4434 ), #1914, .T. ) ;
#142=CARTESIAN_POINT ( 'NONE',  ( 18.53245405280430802, -27.00737899243800300, 8.462064221501000461 ) ) ;
#143=ORIENTED_EDGE ( 'NONE', *, *, #1430, .T. ) ;
#147=DIRECTION ( 'NONE',  ( -1.000000000000000000, 1.499759782661860071E-32, -1.224646799147350002E-16 ) ) ;
#155=DIRECTION ( 'NONE',  ( 0.000000000000000000, 0.000000000000000000, 1.000000000000000000 ) ) ;
#158=VECTOR ( 'NONE', #4649, 1000.000000000000000 ) ;
#161=ORIENTED_EDGE ( 'NONE', *, *, #9054, .T. ) ;
#164=DIRECTION ( 'NONE',  ( 0.000000000000000000, 1.131341397376178572E-16, -1.000000000000000000 ) ) ;
#170=ORIENTED_EDGE ( 'NONE', *, *, #333, .F. ) ;
#179=CARTESIAN_POINT ( 'NONE',  ( -15.49969986081099371, -9.007378992438001220, -13.28793577849899599 ) ) ;
#180=CARTESIAN_POINT ( 'NONE',  ( -28.78282149594069850, -32.00737899243799944, 24.21206422150099868 ) ) ;
#181=EDGE_CURVE ( 'NONE', #13469, #7197, #14834, .T. ) ;
#184=ORIENTED_EDGE ( 'NONE', *, *, #9513, .F. ) ;
#198=EDGE_CURVE ( 'NONE', #14370, #12333, #7164, .T. ) ;
#200=CARTESIAN_POINT ( 'NONE',  ( -15.49969986081099904, -19.50737899243800300, 24.21206422150100224 ) ) ;
#201=AXIS2_PLACEMENT_3D ( 'NONE', #9207, #12513, #13890 ) ;
#205=AXIS2_PLACEMENT_3D ( 'NONE', #2653, #1576, #13144 ) ;
#209=CARTESIAN_POINT ( 'NONE',  ( 7.464989229556169725, 4.086072560925113173, 25.52420958079008884 ) ) ;
#216=DIRECTION ( 'NONE',  ( 0.000000000000000000, 0.000000000000000000, 1.000000000000000000 ) ) ;
#219=PLANE ( 'NONE',  #12030 ) ;
#220=CARTESIAN_POINT ( 'NONE',  ( -15.49969986081099904, 0.9926210075619987805, 24.21206422150099868 ) ) ;
#222=VECTOR ( 'NONE', #14585, 1000.000000000000000 ) ;
#233=DIRECTION ( 'NONE',  ( 0.000000000000000000, 0.000000000000000000, 1.000000000000000000 ) ) ;
#241=ORIENTED_EDGE ( 'NONE', *, *, #492, .T. ) ;
#248=EDGE_CURVE ( 'NONE', #9045, #3429, #2887, .T. ) ;
#249=PLANE ( 'NONE',  #11119 ) ;
#258=SURFACE_SIDE_STYLE ('',( #7350 ) ) ;
#259=VERTEX_POINT ( 'NONE', #1213 ) ;
#265=DIRECTION ( 'NONE',  ( 0.000000000000000000, 0.000000000000000000, 1.000000000000000000 ) ) ;
#268=DIRECTION ( 'NONE',  ( 0.000000000000000000, 1.224646799147350002E-16, -1.000000000000000000 ) ) ;
#271=DIRECTION ( 'NONE',  ( 1.000000000000000000, -3.922012711866029438E-32, 3.202566417187950042E-16 ) ) ;
#274=EDGE_LOOP ( 'NONE', ( #8027, #11892 ) ) ;
#278=CARTESIAN_POINT ( 'NONE',  ( 21.96528021387864271, -29.82714745920393185, 22.58218370277269571 ) ) ;
#287=CARTESIAN_POINT ( 'NONE',  ( -15.49969986081099904, -32.00737899243799944, 24.21206422150100224 ) ) ;
#292=CARTESIAN_POINT ( 'NONE',  ( 4.500300139189000959, -19.50737899243801010, 55.93350807262470425 ) ) ;
#293=CARTESIAN_POINT ( 'NONE',  ( 0.8003001391889992266, 11.99262100756199878, 24.26206422150100295 ) ) ;
#296=DIRECTION ( 'NONE',  ( 0.000000000000000000, 1.000000000000000000, 1.224646799147350002E-16 ) ) ;
#301=VECTOR ( 'NONE', #1890, 1000.000000000000000 ) ;
#312=DIRECTION ( 'NONE',  ( 1.000000000000000000, -3.922012711866029438E-32, 3.202566417187950042E-16 ) ) ;
#324=( BOUNDED_CURVE ( )  B_SPLINE_CURVE ( 3, ( #292, #8307, #2730, #6008 ),
 .UNSPECIFIED., .F., .T. ) 
 B_SPLINE_CURVE_WITH_KNOTS ( ( 4, 4 ),
 ( 1.008260082251040135, 1.208720131788790120 ),
 .UNSPECIFIED. ) 
 CURVE ( )  GEOMETRIC_REPRESENTATION_ITEM ( )  RATIONAL_B_SPLINE_CURVE ( ( 1.000000000000000000, 0.9966541165307394312, 0.9966541165307394312, 1.000000000000000000 ) ) 
 REPRESENTATION_ITEM ( '' )  );
#331=CARTESIAN_POINT ( 'NONE',  ( -16.66466864975539153, -9.150908980254410352, -13.27094003038157943 ) ) ;
#332=B_SPLINE_CURVE_WITH_KNOTS ( 'NONE', 3,
 ( #3786, #14269, #2413, #7056, #11734, #2637, #7211, #5838 ),
 .UNSPECIFIED., .F., .F.,
 ( 4, 2, 2, 4 ),
 ( 0.000000000000000000, 0.2500000000000007216, 0.5000000000000014433, 1.000000000000000000 ),
 .UNSPECIFIED. ) ;
#333=EDGE_CURVE ( 'NONE', #11915, #14532, #10956, .T. ) ;
#334=EDGE_CURVE ( 'NONE', #9332, #3237, #5095, .T. ) ;
#339=CONICAL_SURFACE ( 'NONE', #2284, 1664.279482350500075, 1.029744258676650093 ) ;
#340=ORIENTED_EDGE ( 'NONE', *, *, #454, .F. ) ;
#345=CARTESIAN_POINT ( 'NONE',  ( -15.49969986081099904, -32.00737899243799944, 24.21206422150100224 ) ) ;
#357=ORIENTED_EDGE ( 'NONE', *, *, #4575, .F. ) ;
#360=ORIENTED_EDGE ( 'NONE', *, *, #12281, .T. ) ;
#364=VERTEX_POINT ( 'NONE', #963 ) ;
#365=CARTESIAN_POINT ( 'NONE',  ( 2.374542637206501272, 7.183219930803497633, 17.76912582958182085 ) ) ;
#367=CARTESIAN_POINT ( 'NONE',  ( 7.367243934124074300, 4.365428709207489710, 26.75804073331549304 ) ) ;
#372=EDGE_CURVE ( 'NONE', #4377, #1107, #9059, .T. ) ;
#377=EDGE_LOOP ( 'NONE', ( #6122, #12748, #11270, #7433 ) ) ;
#381=EDGE_LOOP ( 'NONE', ( #709, #10098 ) ) ;
#385=DIRECTION ( 'NONE',  ( -1.000000000000000000, 0.000000000000000000, 0.000000000000000000 ) ) ;
#388=EDGE_CURVE ( 'NONE', #12884, #3001, #2110, .T. ) ;
#389=ORIENTED_EDGE ( 'NONE', *, *, #14266, .F. ) ;
#404=CARTESIAN_POINT ( 'NONE',  ( -14.19604964772364220, -3.572340267249467960, 61.69496804699286940 ) ) ;
#405=DIRECTION ( 'NONE',  ( 0.000000000000000000, 0.000000000000000000, -1.000000000000000000 ) ) ;
#409=ORIENTED_EDGE ( 'NONE', *, *, #7322, .F. ) ;
#416=ORIENTED_EDGE ( 'NONE', *, *, #10394, .T. ) ;
#418=EDGE_CURVE ( 'NONE', #12386, #5342, #12547, .T. ) ;
#419=DIRECTION ( 'NONE',  ( 0.000000000000000000, -1.000000000000000000, -1.224646799147350002E-16 ) ) ;
#425=CARTESIAN_POINT ( 'NONE',  ( -36.12103303905597329, 5.873878172627213345, 19.00766998042008993 ) ) ;
#429=CARTESIAN_POINT ( 'NONE',  ( -25.49948389380865166, -14.04222171988956980, 60.35420473814775733 ) ) ;
#433=ORIENTED_EDGE ( 'NONE', *, *, #11484, .F. ) ;
#441=AXIS2_PLACEMENT_3D ( 'NONE', #10410, #13028, #12801 ) ;
#444=DIRECTION ( 'NONE',  ( 0.000000000000000000, -2.168404344971007882E-16, 1.000000000000000000 ) ) ;
#445=EDGE_LOOP ( 'NONE', ( #12637, #4168, #4808, #409 ) ) ;
#448=ORIENTED_EDGE ( 'NONE', *, *, #2178, .F. ) ;
#453=VECTOR ( 'NONE', #13350, 1000.000000000000000 ) ;
#454=EDGE_CURVE ( 'NONE', #4959, #9649, #332, .T. ) ;
#460=CARTESIAN_POINT ( 'NONE',  ( 18.30059761021155040, -28.74139264981273456, 7.969802569063922704 ) ) ;
#465=ORIENTED_EDGE ( 'NONE', *, *, #14636, .T. ) ;
#476=EDGE_CURVE ( 'NONE', #15009, #8801, #12188, .T. ) ;
#484=CARTESIAN_POINT ( 'NONE',  ( 22.00030013918900096, -27.00737899243800300, 27.46206422150099868 ) ) ;
#490=ORIENTED_EDGE ( 'NONE', *, *, #13327, .T. ) ;
#492=EDGE_CURVE ( 'NONE', #11705, #3542, #8135, .T. ) ;
#493=VECTOR ( 'NONE', #2962, 1000.000000000000000 ) ;
#499=DIRECTION ( 'NONE',  ( 0.000000000000000000, -1.000000000000000000, -1.224646799147350002E-16 ) ) ;
#509=CARTESIAN_POINT ( 'NONE',  ( 4.185908152460800835, 11.99262100756689620, 32.26206422150099939 ) ) ;
#510=CARTESIAN_POINT ( 'NONE',  ( 13.85920135429429934, -23.75737899243800300, 43.21206422150100224 ) ) ;
#511=ORIENTED_EDGE ( 'NONE', *, *, #9818, .F. ) ;
#513=CARTESIAN_POINT ( 'NONE',  ( -33.37394235882850069, 7.183219930803497633, 30.65500261342018007 ) ) ;
#516=CARTESIAN_POINT ( 'NONE',  ( 21.99139210015182755, -23.86155550811809078, 25.05589765920358403 ) ) ;
#528=CARTESIAN_POINT ( 'NONE',  ( 6.045543233663400073, 12.99262100756199878, 32.26206422150099939 ) ) ;
#535=EDGE_LOOP ( 'NONE', ( #3862, #9614, #2971, #6742 ) ) ;
#540=CARTESIAN_POINT ( 'NONE',  ( -33.06833922757078881, 8.472784761962646627, 16.97712202220791156 ) ) ;
#543=CONICAL_SURFACE ( 'NONE', #12526, 23.00000000000000000, 1.047197551196598297 ) ;
#545=B_SPLINE_CURVE_WITH_KNOTS ( 'NONE', 3,
 ( #4916, #1388, #10721, #3763 ),
 .UNSPECIFIED., .F., .F.,
 ( 4, 4 ),
 ( 0.000000000000000000, 1.000000000000000000 ),
 .UNSPECIFIED. ) ;
#549=EDGE_CURVE ( 'NONE', #3237, #9332, #11203, .T. ) ;
#554=ORIENTED_EDGE ( 'NONE', *, *, #8317, .F. ) ;
#558=EDGE_CURVE ( 'NONE', #9278, #700, #3139, .T. ) ;
#559=DIRECTION ( 'NONE',  ( 0.000000000000000000, 1.508455196501571429E-16, -1.000000000000000000 ) ) ;
#562=EDGE_CURVE ( 'NONE', #12498, #8595, #5230, .T. ) ;
#563=PLANE ( 'NONE',  #11485 ) ;
#566=CARTESIAN_POINT ( 'NONE',  ( -31.79969986081099975, 3.992621007561997892, 24.21206422150099868 ) ) ;
#567=CARTESIAN_POINT ( 'NONE',  ( -36.32388817133784897, 5.776599650201116098, 19.12436011050695939 ) ) ;
#581=AXIS2_PLACEMENT_3D ( 'NONE', #11592, #5841, #967 ) ;
#582=CARTESIAN_POINT ( 'NONE',  ( 4.847130973315482372, 6.005480809351509741, 18.85628166566612407 ) ) ;
#587=CARTESIAN_POINT ( 'NONE',  ( -19.99969986081099904, -13.50737899243800122, 6.712064221500998684 ) ) ;
#594=CARTESIAN_POINT ( 'NONE',  ( 21.89436017916797894, -25.37669890083672541, 21.39281022185563330 ) ) ;
#609=VERTEX_POINT ( 'NONE', #5087 ) ;
#620=CARTESIAN_POINT ( 'NONE',  ( -15.49969986081099904, 22.99262100756200056, 24.21206422150099868 ) ) ;
#630=ORIENTED_EDGE ( 'NONE', *, *, #6574, .F. ) ;
#634=CARTESIAN_POINT ( 'NONE',  ( -12.52412891130166628, -10.11885649493944150, -13.17027540314590794 ) ) ;
#641=CARTESIAN_POINT ( 'NONE',  ( -33.37394235882850069, 7.183219930803497633, 17.76912582958182085 ) ) ;
#647=FACE_OUTER_BOUND ( 'NONE', #4000, .T. ) ;
#650=EDGE_CURVE ( 'NONE', #1508, #1539, #12937, .T. ) ;
#651=DIRECTION ( 'NONE',  ( 0.000000000000000000, 1.000000000000000000, 1.224646799147350002E-16 ) ) ;
#663=CARTESIAN_POINT ( 'NONE',  ( 21.85920135429435618, -26.79521804582964251, 20.96206422150099868 ) ) ;
#665=ORIENTED_EDGE ( 'NONE', *, *, #13327, .F. ) ;
#676=CARTESIAN_POINT ( 'NONE',  ( 13.85920135429429934, -27.00737899243800300, 46.46206422150100224 ) ) ;
#691=CARTESIAN_POINT ( 'NONE',  ( -15.49968909271368211, -3.507379016232285096, 61.71092834827113194 ) ) ;
#700=VERTEX_POINT ( 'NONE', #2286 ) ;
#708=DIRECTION ( 'NONE',  ( 0.000000000000000000, 0.000000000000000000, 1.000000000000000000 ) ) ;
#709=ORIENTED_EDGE ( 'NONE', *, *, #4943, .T. ) ;
#713=AXIS2_PLACEMENT_3D ( 'NONE', #10885, #7580, #9736 ) ;
#722=EDGE_LOOP ( 'NONE', ( #6651, #10903 ) ) ;
#723=EDGE_CURVE ( 'NONE', #11355, #1607, #5563, .T. ) ;
#726=AXIS2_PLACEMENT_3D ( 'NONE', #13566, #10336, #938 ) ;
#730=DIRECTION ( 'NONE',  ( 0.000000000000000000, 1.000000000000000000, 0.000000000000000000 ) ) ;
#732=CARTESIAN_POINT ( 'NONE',  ( 5.426450521647101510, 12.65779542994580353, 16.16206422150100153 ) ) ;
#740=EDGE_CURVE ( 'NONE', #13270, #11202, #9081, .T. ) ;
#742=CARTESIAN_POINT ( 'NONE',  ( 21.97315826285361595, -24.08605709633378567, 25.65191965223944237 ) ) ;
#750=CARTESIAN_POINT ( 'NONE',  ( -15.49969986081099904, -13.50737899243800122, 61.71206422150099513 ) ) ;
#763=ORIENTED_EDGE ( 'NONE', *, *, #11807, .F. ) ;
#770=FACE_OUTER_BOUND ( 'NONE', #1435, .T. ) ;
#774=CARTESIAN_POINT ( 'NONE',  ( 17.02198936008371533, -30.24703833648301554, 42.88401681784144870 ) ) ;
#778=VECTOR ( 'NONE', #1871, 1000.000000000000000 ) ;
#779=ADVANCED_FACE ( 'NONE', ( #2362 ), #6997, .T. ) ;
#781=CARTESIAN_POINT ( 'NONE',  ( 2.105912444148304807, 8.250019247675099976, 17.06248425561910409 ) ) ;
#794=CIRCLE ( 'NONE', #4212, 5.250000000000000888 ) ;
#810=CARTESIAN_POINT ( 'NONE',  ( 6.045543233663400073, 12.99262100756199878, 16.16206422150100153 ) ) ;
#813=CARTESIAN_POINT ( 'NONE',  ( -35.18530787408519700, 11.99262100756819827, 32.26206422150099939 ) ) ;
#816=LINE ( 'NONE', #4179, #222 ) ;
#820=CARTESIAN_POINT ( 'NONE',  ( 2.374542637206501272, 7.183219930803497633, 30.65500261342018007 ) ) ;
#821=VECTOR ( 'NONE', #9559, 1000.000000000000000 ) ;
#837=VECTOR ( 'NONE', #3403, 1000.000000000000000 ) ;
#838=EDGE_LOOP ( 'NONE', ( #10150, #10101, #7348, #913, #13152 ) ) ;
#847=EDGE_CURVE ( 'NONE', #10705, #1908, #4099, .T. ) ;
#849=EDGE_CURVE ( 'NONE', #6240, #10757, #14803, .T. ) ;
#859=CARTESIAN_POINT ( 'NONE',  ( 6.045543233663400073, 0.9926210075619987805, 16.16206422150100153 ) ) ;
#874=ORIENTED_EDGE ( 'NONE', *, *, #9818, .T. ) ;
#876=DIRECTION ( 'NONE',  ( 0.000000000000000000, -1.000000000000000000, -1.224646799147350002E-16 ) ) ;
#881=CYLINDRICAL_SURFACE ( 'NONE', #14903, 8.000000000000000000 ) ;
#882=CARTESIAN_POINT ( 'NONE',  ( 2.436724872642413331, 11.05255549920696012, 16.20867245923580313 ) ) ;
#884=CARTESIAN_POINT ( 'NONE',  ( 15.61764008820435023, -24.36042187135127080, 3.281355806888882398 ) ) ;
#887=CARTESIAN_POINT ( 'NONE',  ( 3.683561516709968675, 6.562241739470401569, 30.13885157671532156 ) ) ;
#895=AXIS2_PLACEMENT_3D ( 'NONE', #13622, #13924, #1219 ) ;
#899=ADVANCED_FACE ( 'NONE', ( #8979, #11140 ), #4029, .T. ) ;
#901=DIRECTION ( 'NONE',  ( -1.000000000000000000, 0.000000000000000000, 0.000000000000000000 ) ) ;
#908=VECTOR ( 'NONE', #6585, 1000.000000000000000 ) ;
#913=ORIENTED_EDGE ( 'NONE', *, *, #997, .F. ) ;
#925=DIRECTION ( 'NONE',  ( 0.000000000000000000, 0.000000000000000000, 1.000000000000000000 ) ) ;
#929=CARTESIAN_POINT ( 'NONE',  ( 15.30759700337437046, -29.22784282607966588, 45.59414329854286763 ) ) ;
#930=ORIENTED_EDGE ( 'NONE', *, *, #418, .T. ) ;
#938=DIRECTION ( 'NONE',  ( 0.000000000000000000, 0.000000000000000000, -1.000000000000000000 ) ) ;
#939=ADVANCED_FACE ( 'NONE', ( #1653 ), #8885, .T. ) ;
#945=CIRCLE ( 'NONE', #13899, 8.000000000000000000 ) ;
#947=VERTEX_POINT ( 'NONE', #2336 ) ;
#948=CARTESIAN_POINT ( 'NONE',  ( 17.85343114739217540, -24.33247860872462809, 41.35438736840348639 ) ) ;
#953=AXIS2_PLACEMENT_3D ( 'NONE', #1340, #3709, #1183 ) ;
#962=CARTESIAN_POINT ( 'NONE',  ( -15.49969986081099904, 1010.738102757665843, 24.21206422150112303 ) ) ;
#963=CARTESIAN_POINT ( 'NONE',  ( 9.000300139189000959, -27.00737899243800300, 26.71206422150099868 ) ) ;
#967=DIRECTION ( 'NONE',  ( 0.000000000000000000, -1.508455196501571676E-16, 1.000000000000000000 ) ) ;
#969=VECTOR ( 'NONE', #11746, 1000.000000000000114 ) ;
#970=VERTEX_POINT ( 'NONE', #7821 ) ;
#973=DIRECTION ( 'NONE',  ( 0.000000000000000000, 0.000000000000000000, 1.000000000000000000 ) ) ;
#977=VECTOR ( 'NONE', #12742, 1000.000000000000000 ) ;
#980=EDGE_CURVE ( 'NONE', #8879, #2383, #6903, .T. ) ;
#981=CARTESIAN_POINT ( 'NONE',  ( 7.000300139189000070, -19.50737899243800300, 24.21206422150099868 ) ) ;
#986=CARTESIAN_POINT ( 'NONE',  ( -37.63784331376448478, 5.145091203786375189, 28.44116034148276739 ) ) ;
#994=FACE_OUTER_BOUND ( 'NONE', #2243, .T. ) ;
#997=EDGE_CURVE ( 'NONE', #947, #12931, #5539, .T. ) ;
#1002=CARTESIAN_POINT ( 'NONE',  ( 18.17361288855373758, -29.10044277972165716, 40.71597190168268554 ) ) ;
#1011=AXIS2_PLACEMENT_3D ( 'NONE', #9587, #2275, #13121 ) ;
#1024=AXIS2_PLACEMENT_3D ( 'NONE', #8503, #14327, #12179 ) ;
#1025=DIRECTION ( 'NONE',  ( 0.000000000000000000, 1.000000000000000000, 1.224646799147350002E-16 ) ) ;
#1030=VECTOR ( 'NONE', #2943, 1000.000000000000000 ) ;
#1040=CARTESIAN_POINT ( 'NONE',  ( -15.49969986081099904, 10.68321993080349941, 5.212064221501000461 ) ) ;
#1042=ORIENTED_EDGE ( 'NONE', *, *, #4702, .F. ) ;
#1046=AXIS2_PLACEMENT_3D ( 'NONE', #5420, #4205, #7634 ) ;
#1047=ORIENTED_EDGE ( 'NONE', *, *, #2055, .T. ) ;
#1052=ADVANCED_FACE ( 'NONE', ( #6135 ), #8210, .T. ) ;
#1053=CIRCLE ( 'NONE', #8629, 37.50000000000000000 ) ;
#1077=CARTESIAN_POINT ( 'NONE',  ( 7.471063718837686274, 4.067408198524465668, 22.89737889731558340 ) ) ;
#1079=FACE_BOUND ( 'NONE', #11723, .T. ) ;
#1080=ORIENTED_EDGE ( 'NONE', *, *, #198, .T. ) ;
#1082=DIRECTION ( 'NONE',  ( -1.000000000000000000, 1.499759782661860071E-32, -1.224646799147350002E-16 ) ) ;
#1089=FACE_BOUND ( 'NONE', #8600, .T. ) ;
#1091=CARTESIAN_POINT ( 'NONE',  ( 18.10099741743264445, -24.75028974787160507, 40.86364982085049036 ) ) ;
#1100=ADVANCED_FACE ( 'NONE', ( #1337 ), #2635, .F. ) ;
#1107=VERTEX_POINT ( 'NONE', #9441 ) ;
#1109=DIRECTION ( 'NONE',  ( 0.000000000000000000, 1.131341397376178572E-16, -1.000000000000000000 ) ) ;
#1117=EDGE_CURVE ( 'NONE', #8216, #15087, #8160, .T. ) ;
#1126=CARTESIAN_POINT ( 'NONE',  ( -38.20013690429809827, 4.873818854045000037, 27.91208557747711083 ) ) ;
#1128=DIRECTION ( 'NONE',  ( 0.000000000000000000, -1.000000000000000000, -1.224646799147350002E-16 ) ) ;
#1131=ORIENTED_EDGE ( 'NONE', *, *, #12720, .F. ) ;
#1133=CARTESIAN_POINT ( 'NONE',  ( -15.49969986081099904, -13.50737899243800122, 6.712064221500998684 ) ) ;
#1135=DIRECTION ( 'NONE',  ( 0.000000000000000000, -1.000000000000000000, -1.224646799147350002E-16 ) ) ;
#1136=AXIS2_PLACEMENT_3D ( 'NONE', #6177, #8477, #6325 ) ;
#1148=FACE_OUTER_BOUND ( 'NONE', #8288, .T. ) ;
#1150=VERTEX_POINT ( 'NONE', #10591 ) ;
#1155=CARTESIAN_POINT ( 'NONE',  ( 7.000300139189000070, -19.50737899243799589, -5.787935778498998651 ) ) ;
#1159=CARTESIAN_POINT ( 'NONE',  ( 17.56517143204546372, -24.02498291609396119, 6.519892126142639022 ) ) ;
#1172=ORIENTED_EDGE ( 'NONE', *, *, #8951, .F. ) ;
#1174=CONICAL_SURFACE ( 'NONE', #2147, 19.00000000000000000, 1.047197551196598297 ) ;
#1176=VECTOR ( 'NONE', #6633, 1000.000000000000000 ) ;
#1183=DIRECTION ( 'NONE',  ( 0.000000000000000000, 0.000000000000000000, 1.000000000000000000 ) ) ;
#1189=ORIENTED_EDGE ( 'NONE', *, *, #7592, .F. ) ;
#1191=ADVANCED_FACE ( 'NONE', ( #13053 ), #10614, .T. ) ;
#1196=AXIS2_PLACEMENT_3D ( 'NONE', #14185, #13126, #13050 ) ;
#1199=CIRCLE ( 'NONE', #14634, 37.50000000000000000 ) ;
#1202=DIRECTION ( 'NONE',  ( 0.000000000000000000, -1.000000000000000000, -1.224646799147350002E-16 ) ) ;
#1204=DIRECTION ( 'NONE',  ( 0.000000000000000000, 0.000000000000000000, 1.000000000000000000 ) ) ;
#1213=CARTESIAN_POINT ( 'NONE',  ( -15.49969986081099904, -2.007378992437998111, -3.787935778499002204 ) ) ;
#1219=DIRECTION ( 'NONE',  ( 0.000000000000000000, 2.168404344971008868E-16, -1.000000000000000000 ) ) ;
#1220=EDGE_CURVE ( 'NONE', #14257, #7843, #4288, .T. ) ;
#1222=EDGE_CURVE ( 'NONE', #1625, #1508, #11426, .T. ) ;
#1231=CIRCLE ( 'NONE', #9782, 6.250000000000001776 ) ;
#1241=ORIENTED_EDGE ( 'NONE', *, *, #13662, .T. ) ;
#1247=VERTEX_POINT ( 'NONE', #4441 ) ;
#1249=CARTESIAN_POINT ( 'NONE',  ( 22.00030013918900096, -27.00737899243800300, 24.21206422150099868 ) ) ;
#1251=FACE_OUTER_BOUND ( 'NONE', #10605, .T. ) ;
#1257=ORIENTED_EDGE ( 'NONE', *, *, #7736, .F. ) ;
#1259=CARTESIAN_POINT ( 'NONE',  ( -19.97045281939299954, -14.09771657249876142, -13.02052492037858933 ) ) ;
#1261=ORIENTED_EDGE ( 'NONE', *, *, #492, .F. ) ;
#1262=CARTESIAN_POINT ( 'NONE',  ( 21.99148493447345132, -30.15430098416778648, 25.05124702636123146 ) ) ;
#1266=VERTEX_POINT ( 'NONE', #5653 ) ;
#1268=VECTOR ( 'NONE', #9947, 1000.000000000000000 ) ;
#1279=VECTOR ( 'NONE', #13433, 1000.000000000000000 ) ;
#1281=DIRECTION ( 'NONE',  ( 0.000000000000000000, 1.224646799147350002E-16, -1.000000000000000000 ) ) ;
#1282=EDGE_LOOP ( 'NONE', ( #9084, #8815, #10468, #11123, #3395 ) ) ;
#1286=CARTESIAN_POINT ( 'NONE',  ( 6.045543233663400073, 3.992621007561997892, 24.26206422150100295 ) ) ;
#1290=DIRECTION ( 'NONE',  ( 0.000000000000000000, -0.9895257890689694857, 0.1443562010009729335 ) ) ;
#1294=CARTESIAN_POINT ( 'NONE',  ( -6.519606984562681617, -17.91311303219895024, 60.62118659065755111 ) ) ;
#1303=ORIENTED_EDGE ( 'NONE', *, *, #10829, .T. ) ;
#1307=B_SPLINE_CURVE_WITH_KNOTS ( 'NONE', 3,
 ( #7540, #663, #8621, #14437, #14587, #6462, #594, #13306, #1891, #1661, #2882, #3106, #7465, #12142, #10993, #4182, #12220, #6313, #5109, #516, #6538, #742, #1731, #8765, #8836, #4036, #5176, #7765, #5256, #14516, #9848, #1816, #8689, #13371 ),
 .UNSPECIFIED., .F., .F.,
 ( 4, 2, 2, 2, 2, 2, 2, 2, 2, 2, 2, 2, 2, 2, 2, 2, 4 ),
 ( 0.01024809238176392634, 0.01088874702714459804, 0.01152940167252526973, 0.01217005631790594143, 0.01281071096328661313, 0.01345136560866728656, 0.01409202025404795826, 0.01473267489942862996, 0.01537332954480930165, 0.01601398419018997335, 0.01665463883557064678, 0.01729529348095131674, 0.01793594812633199018, 0.01857660277171266361, 0.01921725741709333357, 0.01985791206247400353, 0.02049856670785467697 ),
 .UNSPECIFIED. ) ;
#1312=AXIS2_PLACEMENT_3D ( 'NONE', #13815, #9136, #1109 ) ;
#1317=EDGE_CURVE ( 'NONE', #3567, #2643, #6642, .T. ) ;
#1322=DIRECTION ( 'NONE',  ( 0.000000000000000000, 0.000000000000000000, 1.000000000000000000 ) ) ;
#1324=CARTESIAN_POINT ( 'NONE',  ( -11.92171335822600042, -16.25216409852338373, -13.11721111237203630 ) ) ;
#1327=VECTOR ( 'NONE', #6528, 1000.000000000000000 ) ;
#1337=FACE_OUTER_BOUND ( 'NONE', #4258, .T. ) ;
#1340=CARTESIAN_POINT ( 'NONE',  ( -15.49969986081099904, 64.39262100756199914, 24.21206422150100579 ) ) ;
#1343=CARTESIAN_POINT ( 'NONE',  ( -24.47770327408855806, -17.91589678518842277, 60.62170142699616804 ) ) ;
#1346=CARTESIAN_POINT ( 'NONE',  ( 21.94844983914712344, -29.59392153401264380, 26.19129280141764937 ) ) ;
#1365=DIRECTION ( 'NONE',  ( 0.000000000000000000, 1.000000000000000000, 1.224646799147350002E-16 ) ) ;
#1367=DIRECTION ( 'NONE',  ( 0.000000000000000000, -1.000000000000000000, -1.224646799147350002E-16 ) ) ;
#1369=EDGE_CURVE ( 'NONE', #7843, #12569, #3122, .T. ) ;
#1373=ORIENTED_EDGE ( 'NONE', *, *, #8795, .T. ) ;
#1379=CARTESIAN_POINT ( 'NONE',  ( 7.246718728573819490, 4.729174316162667147, 20.79414966637559914 ) ) ;
#1380=VERTEX_POINT ( 'NONE', #3370 ) ;
#1388=CARTESIAN_POINT ( 'NONE',  ( -33.43612459436373996, 11.05255549926123493, 16.20867245922678990 ) ) ;
#1391=B_SPLINE_CURVE_WITH_KNOTS ( 'NONE', 3,
 ( #11818, #7214, #9599, #1343, #5994, #10901, #9521, #3940, #7295, #2791, #429, #2716 ),
 .UNSPECIFIED., .F., .F.,
 ( 4, 2, 2, 2, 2, 4 ),
 ( 0.000000000000000000, 0.03633466677368843434, 0.05450200016053259600, 0.07266933354737674378, 0.1090040003210653030, 0.1453386670947538206 ),
 .UNSPECIFIED. ) ;
#1393=CARTESIAN_POINT ( 'NONE',  ( 22.00030013918900096, -27.00737899243800300, 43.21206422150100224 ) ) ;
#1397=ORIENTED_EDGE ( 'NONE', *, *, #15002, .F. ) ;
#1398=ORIENTED_EDGE ( 'NONE', *, *, #6504, .F. ) ;
#1400=VERTEX_POINT ( 'NONE', #10400 ) ;
#1423=CARTESIAN_POINT ( 'NONE',  ( 21.98624202466326238, -30.09200759101065614, 25.25752346147605820 ) ) ;
#1424=AXIS2_PLACEMENT_3D ( 'NONE', #4250, #12289, #2950 ) ;
#1428=FACE_OUTER_BOUND ( 'NONE', #3168, .T. ) ;
#1429=B_SPLINE_CURVE_WITH_KNOTS ( 'NONE', 3,
 ( #4750, #1379, #7098, #10712, #3678, #1077, #5878, #9561 ),
 .UNSPECIFIED., .F., .F.,
 ( 4, 2, 2, 4 ),
 ( 0.000000000000000000, 0.2499999999999993894, 0.4999999999999987788, 1.000000000000000000 ),
 .UNSPECIFIED. ) ;
#1430=EDGE_CURVE ( 'NONE', #3542, #8123, #8406, .T. ) ;
#1435=EDGE_LOOP ( 'NONE', ( #12352, #4053, #12715, #5829, #11865, #12279, #4757 ) ) ;
#1445=FACE_OUTER_BOUND ( 'NONE', #274, .T. ) ;
#1446=VECTOR ( 'NONE', #6854, 1000.000000000000000 ) ;
#1450=CARTESIAN_POINT ( 'NONE',  ( 17.25070158960591016, -30.18020639231665925, 5.944247395788684329 ) ) ;
#1457=AXIS2_PLACEMENT_3D ( 'NONE', #10103, #4303, #8956 ) ;
#1459=FACE_OUTER_BOUND ( 'NONE', #4180, .T. ) ;
#1469=CARTESIAN_POINT ( 'NONE',  ( 18.35447865076064744, -25.46704448935311760, 8.082739883746024034 ) ) ;
#1473=CARTESIAN_POINT ( 'NONE',  ( -13.24180272517058654, -17.41093464048234551, -13.22069529846239888 ) ) ;
#1479=ORIENTED_EDGE ( 'NONE', *, *, #3283, .T. ) ;
#1487=CIRCLE ( 'NONE', #9294, 15.87500000000000355 ) ;
#1492=ORIENTED_EDGE ( 'NONE', *, *, #6404, .T. ) ;
#1500=CYLINDRICAL_SURFACE ( 'NONE', #1570, 3.249999999999999556 ) ;
#1508=VERTEX_POINT ( 'NONE', #9711 ) ;
#1515=DIRECTION ( 'NONE',  ( -1.000000000000000000, 0.000000000000000000, 0.000000000000000000 ) ) ;
#1518=CIRCLE ( 'NONE', #1024, 19.00000000000000000 ) ;
#1527=CARTESIAN_POINT ( 'NONE',  ( 15.96592141709277790, -29.94643662871589029, 3.810787175452606146 ) ) ;
#1530=DIRECTION ( 'NONE',  ( 0.000000000000000000, -1.000000000000000000, -1.224646799147350002E-16 ) ) ;
#1531=CARTESIAN_POINT ( 'NONE',  ( 2.143005335038563608, 8.120575443056516463, 31.26488582106640024 ) ) ;
#1539=VERTEX_POINT ( 'NONE', #13464 ) ;
#1545=AXIS2_PLACEMENT_3D ( 'NONE', #4527, #15074, #2156 ) ;
#1546=PLANE ( 'NONE',  #10322 ) ;
#1547=DIRECTION ( 'NONE',  ( 0.000000000000000000, 0.5150380749100579303, 0.8571673007021101132 ) ) ;
#1551=PRESENTATION_STYLE_ASSIGNMENT (( #7042 ) ) ;
#1552=ORIENTED_EDGE ( 'NONE', *, *, #14224, .F. ) ;
#1556=EDGE_LOOP ( 'NONE', ( #448, #12545, #14683, #10579, #5127, #3544, #6237 ) ) ;
#1557=ORIENTED_EDGE ( 'NONE', *, *, #2972, .T. ) ;
#1561=VECTOR ( 'NONE', #8756, 1000.000000000000000 ) ;
#1567=CARTESIAN_POINT ( 'NONE',  ( -31.79969986081099975, 11.99262100756199878, 24.16206422150099797 ) ) ;
#1569=VERTEX_POINT ( 'NONE', #6553 ) ;
#1570=AXIS2_PLACEMENT_3D ( 'NONE', #2650, #9954, #708 ) ;
#1576=DIRECTION ( 'NONE',  ( 0.000000000000000000, -1.000000000000000000, -1.224646799147350002E-16 ) ) ;
#1579=VERTEX_POINT ( 'NONE', #3200 ) ;
#1589=ORIENTED_EDGE ( 'NONE', *, *, #6607, .T. ) ;
#1590=VECTOR ( 'NONE', #4024, 1000.000000000000000 ) ;
#1592=CARTESIAN_POINT ( 'NONE',  ( -37.04494295528539993, 12.99262100756199878, 16.16206422150100153 ) ) ;
#1598=CARTESIAN_POINT ( 'NONE',  ( 9.000300139189000959, -27.00737899243800300, 43.21206422150100224 ) ) ;
#1607=VERTEX_POINT ( 'NONE', #7074 ) ;
#1624=ORIENTED_EDGE ( 'NONE', *, *, #3004, .T. ) ;
#1625=VERTEX_POINT ( 'NONE', #9155 ) ;
#1626=CARTESIAN_POINT ( 'NONE',  ( -15.49969986081099904, 12.99262100756199878, 24.21206422150099868 ) ) ;
#1638=CIRCLE ( 'NONE', #4825, 8.000000000000003553 ) ;
#1641=ORIENTED_EDGE ( 'NONE', *, *, #13372, .F. ) ;
#1642=ORIENTED_EDGE ( 'NONE', *, *, #12311, .T. ) ;
#1644=VERTEX_POINT ( 'NONE', #2361 ) ;
#1645=AXIS2_PLACEMENT_3D ( 'NONE', #1886, #3101, #7761 ) ;
#1647=CARTESIAN_POINT ( 'NONE',  ( 4.904519586037782375, 5.977956585851564419, 18.88724033448293227 ) ) ;
#1648=FACE_OUTER_BOUND ( 'NONE', #535, .T. ) ;
#1653=FACE_OUTER_BOUND ( 'NONE', #3673, .T. ) ;
#1656=ORIENTED_EDGE ( 'NONE', *, *, #8795, .F. ) ;
#1657=CARTESIAN_POINT ( 'NONE',  ( -31.13003983167857314, -27.07585217469822680, -9.967496158821944618 ) ) ;
#1661=CARTESIAN_POINT ( 'NONE',  ( 21.93915798269402728, -24.55717426787524715, 22.06612857817768969 ) ) ;
#1672=ORIENTED_EDGE ( 'NONE', *, *, #93, .F. ) ;
#1677=ORIENTED_EDGE ( 'NONE', *, *, #8951, .T. ) ;
#1691=AXIS2_PLACEMENT_3D ( 'NONE', #13154, #147, #9464 ) ;
#1692=TOROIDAL_SURFACE ( 'NONE', #10243, 28.00000000000000000, 5.000000000000000000 ) ;
#1694=ORIENTED_EDGE ( 'NONE', *, *, #10377, .F. ) ;
#1695=LINE ( 'NONE', #3991, #10549 ) ;
#1700=ORIENTED_EDGE ( 'NONE', *, *, #1117, .T. ) ;
#1708=VECTOR ( 'NONE', #7051, 1000.000000000000000 ) ;
#1712=CARTESIAN_POINT ( 'NONE',  ( 6.045543233663400073, 0.9926210075619987805, 32.26206422150099939 ) ) ;
#1715=ORIENTED_EDGE ( 'NONE', *, *, #9916, .F. ) ;
#1723=DIRECTION ( 'NONE',  ( 0.000000000000000000, 1.000000000000000000, 1.224646799147350002E-16 ) ) ;
#1724=CARTESIAN_POINT ( 'NONE',  ( 1.760741030006599317, 10.68321993080349763, 32.15417856559049881 ) ) ;
#1730=ORIENTED_EDGE ( 'NONE', *, *, #418, .F. ) ;
#1731=CARTESIAN_POINT ( 'NONE',  ( 21.96532791796805739, -24.18694564958964222, 25.84096742429681726 ) ) ;
#1732=CYLINDRICAL_SURFACE ( 'NONE', #8478, 22.99999999999999645 ) ;
#1737=EDGE_CURVE ( 'NONE', #1827, #4959, #9779, .T. ) ;
#1745=DIRECTION ( 'NONE',  ( 0.000000000000000000, 0.000000000000000000, 1.000000000000000000 ) ) ;
#1752=ORIENTED_EDGE ( 'NONE', *, *, #14125, .F. ) ;
#1755=CARTESIAN_POINT ( 'NONE',  ( -15.49969986081099904, -13.50737899243800122, 6.712064221500998684 ) ) ;
#1760=CARTESIAN_POINT ( 'NONE',  ( -32.89073566799068971, 9.431003388506304930, 16.55506475363483787 ) ) ;
#1765=DIRECTION ( 'NONE',  ( 0.000000000000000000, -1.000000000000000000, -1.224646799147350002E-16 ) ) ;
#1775=ORIENTED_EDGE ( 'NONE', *, *, #8960, .T. ) ;
#1777=EDGE_CURVE ( 'NONE', #5054, #364, #6270, .T. ) ;
#1780=CARTESIAN_POINT ( 'NONE',  ( -15.49969986081099549, 0.9926210075620015560, 1.212064221501000461 ) ) ;
#1782=B_SPLINE_CURVE_WITH_KNOTS ( 'NONE', 3,
 ( #820, #4181, #12015, #1531, #8834, #8916, #12369, #13596, #6184, #2755, #10057, #5476 ),
 .UNSPECIFIED., .F., .F.,
 ( 4, 2, 2, 2, 2, 4 ),
 ( 0.000000000000000000, 0.2500000000000004441, 0.3750000000000000000, 0.4374999999999991673, 0.4999999999999983347, 1.000000000000000000 ),
 .UNSPECIFIED. ) ;
#1784=ADVANCED_FACE ( 'NONE', ( #11995 ), #3879, .F. ) ;
#1799=EDGE_CURVE ( 'NONE', #8578, #14370, #1638, .T. ) ;
#1812=ORIENTED_EDGE ( 'NONE', *, *, #12702, .T. ) ;
#1813=CARTESIAN_POINT ( 'NONE',  ( -33.37651573321840459, -23.18484177525213141, -8.848022433876742809 ) ) ;
#1816=CARTESIAN_POINT ( 'NONE',  ( 21.86105339610482545, -26.58130273022555912, 27.44097045403598401 ) ) ;
#1819=ORIENTED_EDGE ( 'NONE', *, *, #7358, .F. ) ;
#1822=DIRECTION ( 'NONE',  ( 0.8660254037844387076, 0.4999999999999998890, 0.000000000000000000 ) ) ;
#1827=VERTEX_POINT ( 'NONE', #513 ) ;
#1828=CARTESIAN_POINT ( 'NONE',  ( -32.94709454773337143, 9.133458655302877816, 31.73466097731338209 ) ) ;
#1839=AXIS2_PLACEMENT_3D ( 'NONE', #12023, #7569, #10876 ) ;
#1851=ORIENTED_EDGE ( 'NONE', *, *, #11118, .T. ) ;
#1854=CARTESIAN_POINT ( 'NONE',  ( 1.760741030006599317, 10.68321993080349763, 16.26994987741148790 ) ) ;
#1857=CARTESIAN_POINT ( 'NONE',  ( -10.99969986081099904, -13.50737899243800122, -13.01695671647155983 ) ) ;
#1858=DIRECTION ( 'NONE',  ( 0.000000000000000000, 1.000000000000000000, 1.224646799147350002E-16 ) ) ;
#1863=AXIS2_PLACEMENT_3D ( 'NONE', #13846, #15066, #9479 ) ;
#1869=EDGE_LOOP ( 'NONE', ( #3180, #14178, #2700, #3321 ) ) ;
#1870=VERTEX_POINT ( 'NONE', #8913 ) ;
#1871=DIRECTION ( 'NONE',  ( 0.000000000000000000, 1.000000000000000000, 1.224646799147350002E-16 ) ) ;
#1881=LINE ( 'NONE', #2318, #8501 ) ;
#1883=CARTESIAN_POINT ( 'NONE',  ( -31.79969986081099975, 11.99262100756199878, 16.16206422150100153 ) ) ;
#1885=ORIENTED_EDGE ( 'NONE', *, *, #12156, .T. ) ;
#1886=CARTESIAN_POINT ( 'NONE',  ( -15.49969986081099904, 1010.738102757665843, 24.21206422150112303 ) ) ;
#1888=CARTESIAN_POINT ( 'NONE',  ( -15.49969986081099904, -13.50737899243800122, 6.712064221500998684 ) ) ;
#1890=DIRECTION ( 'NONE',  ( -1.000000000000000000, 1.499759782661860071E-32, -1.224646799147350002E-16 ) ) ;
#1891=CARTESIAN_POINT ( 'NONE',  ( 21.92052636685137657, -24.86057730259263820, 21.76261826740604377 ) ) ;
#1908=VERTEX_POINT ( 'NONE', #10055 ) ;
#1911=VECTOR ( 'NONE', #8056, 1000.000000000000000 ) ;
#1914=PLANE ( 'NONE',  #9485 ) ;
#1919=CARTESIAN_POINT ( 'NONE',  ( 22.00030013918900096, -27.00737899243800300, 21.71206422150100224 ) ) ;
#1924=CARTESIAN_POINT ( 'NONE',  ( 14.82734454558327464, -28.13112904194727193, 46.26954949554266250 ) ) ;
#1925=ORIENTED_EDGE ( 'NONE', *, *, #4586, .F. ) ;
#1932=ADVANCED_FACE ( 'NONE', ( #13668 ), #11289, .F. ) ;
#1934=VECTOR ( 'NONE', #10797, 1000.000000000000000 ) ;
#1940=CARTESIAN_POINT ( 'NONE',  ( 18.17382430658342685, -24.91495491142563878, 40.71553431842708903 ) ) ;
#1941=ORIENTED_EDGE ( 'NONE', *, *, #7322, .T. ) ;
#1942=CARTESIAN_POINT ( 'NONE',  ( -15.49969986081099904, 10.68321993080349763, 24.21206422150099868 ) ) ;
#1945=CARTESIAN_POINT ( 'NONE',  ( 21.88637859935752772, -28.44597745863666916, 21.29012428004587676 ) ) ;
#1951=EDGE_CURVE ( 'NONE', #12278, #8801, #816, .T. ) ;
#1955=DIRECTION ( 'NONE',  ( 0.000000000000000000, -2.220446049250313081E-16, 1.000000000000000000 ) ) ;
#1956=CARTESIAN_POINT ( 'NONE',  ( 4.185908152463202470, 11.99262100756819827, 16.16206422150100153 ) ) ;
#1976=CARTESIAN_POINT ( 'NONE',  ( -15.49969986081099904, 2.992621007561997004, 24.21206422150099868 ) ) ;
#1977=DIRECTION ( 'NONE',  ( -1.000000000000000000, 0.000000000000000000, 0.000000000000000000 ) ) ;
#1978=ORIENTED_EDGE ( 'NONE', *, *, #14200, .T. ) ;
#1991=CIRCLE ( 'NONE', #10540, 8.886381701226328644 ) ;
#1992=CARTESIAN_POINT ( 'NONE',  ( 22.00030013918900096, -27.00737899243800300, 5.212064221501000461 ) ) ;
#1996=CARTESIAN_POINT ( 'NONE',  ( 18.30004068436167231, -28.74307097840769742, 40.45547825031584921 ) ) ;
#2001=ORIENTED_EDGE ( 'NONE', *, *, #476, .T. ) ;
#2006=CARTESIAN_POINT ( 'NONE',  ( -7.499699860810999041, -19.50737899243799589, 60.84879442494580104 ) ) ;
#2009=CIRCLE ( 'NONE', #6637, 37.50000000000000000 ) ;
#2013=AXIS2_PLACEMENT_3D ( 'NONE', #14988, #13994, #13770 ) ;
#2016=CARTESIAN_POINT ( 'NONE',  ( 16.55725115840230544, -23.76580534705618675, 43.67529649635483224 ) ) ;
#2021=CYLINDRICAL_SURFACE ( 'NONE', #11768, 22.99999999999999645 ) ;
#2028=CARTESIAN_POINT ( 'NONE',  ( 14.70436407088162767, -26.54712960475821149, 1.986671089746397056 ) ) ;
#2029=CARTESIAN_POINT ( 'NONE',  ( -25.49969986081099904, -13.50737899243799944, 6.712064221500998684 ) ) ;
#2032=CARTESIAN_POINT ( 'NONE',  ( -15.49969986081099904, 64.39262100756199914, 24.21206422150100579 ) ) ;
#2040=EDGE_CURVE ( 'NONE', #13214, #1579, #15053, .T. ) ;
#2041=VECTOR ( 'NONE', #9536, 1000.000000000000000 ) ;
#2055=EDGE_CURVE ( 'NONE', #5382, #947, #7156, .T. ) ;
#2067=ADVANCED_FACE ( 'NONE', ( #9062 ), #3482, .F. ) ;
#2070=CARTESIAN_POINT ( 'NONE',  ( -5.636125951381724342, -11.86928948430367114, 60.39167800444882062 ) ) ;
#2073=EDGE_CURVE ( 'NONE', #6681, #5621, #5936, .T. ) ;
#2090=ORIENTED_EDGE ( 'NONE', *, *, #2040, .T. ) ;
#2100=ORIENTED_EDGE ( 'NONE', *, *, #9855, .F. ) ;
#2110=LINE ( 'NONE', #11436, #1911 ) ;
#2113=CARTESIAN_POINT ( 'NONE',  ( -16.08583582846909721, -17.97886954641662527, -13.28448150985099296 ) ) ;
#2128=CARTESIAN_POINT ( 'NONE',  ( -36.87432072752655898, 5.512834891065107712, 29.00861863932625795 ) ) ;
#2132=DIRECTION ( 'NONE',  ( 0.000000000000000000, 9.251858538542971581E-17, -1.000000000000000000 ) ) ;
#2140=AXIS2_PLACEMENT_3D ( 'NONE', #10612, #216, #11994 ) ;
#2145=DIRECTION ( 'NONE',  ( -1.000000000000000000, 0.000000000000000000, 0.000000000000000000 ) ) ;
#2147=AXIS2_PLACEMENT_3D ( 'NONE', #6754, #11438, #6603 ) ;
#2152=VERTEX_POINT ( 'NONE', #8598 ) ;
#2153=CARTESIAN_POINT ( 'NONE',  ( 18.53245405280428315, -27.23732813736695846, 39.96206422150099513 ) ) ;
#2156=DIRECTION ( 'NONE',  ( 0.000000000000000000, 1.000000000000000000, 0.000000000000000000 ) ) ;
#2158=ORIENTED_EDGE ( 'NONE', *, *, #9814, .T. ) ;
#2161=ORIENTED_EDGE ( 'NONE', *, *, #7090, .T. ) ;
#2163=ADVANCED_FACE ( 'NONE', ( #11978 ), #4939, .F. ) ;
#2164=EDGE_CURVE ( 'NONE', #13375, #2383, #1391, .T. ) ;
#2170=CARTESIAN_POINT ( 'NONE',  ( 18.44256572617712209, -25.88025075299395894, 40.15519541060486830 ) ) ;
#2178=EDGE_CURVE ( 'NONE', #1908, #13484, #91, .T. ) ;
#2184=CARTESIAN_POINT ( 'NONE',  ( 7.200737182676100190, 4.873818854045000037, 27.91208557747711083 ) ) ;
#2188=CARTESIAN_POINT ( 'NONE',  ( -16.66704480552753509, -17.86341950268894152, -13.27088927653592521 ) ) ;
#2192=DIRECTION ( 'NONE',  ( -1.000000000000000000, 0.000000000000000000, 0.000000000000000000 ) ) ;
#2202=AXIS2_PLACEMENT_3D ( 'NONE', #5298, #419, #10029 ) ;
#2206=DIRECTION ( 'NONE',  ( -1.000000000000000000, 0.000000000000000000, 0.000000000000000000 ) ) ;
#2212=VERTEX_POINT ( 'NONE', #13134 ) ;
#2230=EDGE_CURVE ( 'NONE', #4277, #13407, #13346, .T. ) ;
#2233=CARTESIAN_POINT ( 'NONE',  ( -15.49969986081099904, -32.00737899243799944, 24.21206422150100224 ) ) ;
#2241=CARTESIAN_POINT ( 'NONE',  ( -15.49969986081099904, 2.992621007562000557, -3.787935778499000428 ) ) ;
#2243=EDGE_LOOP ( 'NONE', ( #14326, #12234, #4361, #8195 ) ) ;
#2244=DIRECTION ( 'NONE',  ( 0.000000000000000000, -1.000000000000000000, -1.224646799147350002E-16 ) ) ;
#2246=ORIENTED_EDGE ( 'NONE', *, *, #7374, .F. ) ;
#2251=CARTESIAN_POINT ( 'NONE',  ( 13.85920135429429934, -27.00737899243800300, 40.71206422150099513 ) ) ;
#2255=CARTESIAN_POINT ( 'NONE',  ( -15.49969986081099904, 10.68321993080349763, 24.21206422150099868 ) ) ;
#2265=CARTESIAN_POINT ( 'NONE',  ( -15.79357609952228714, -18.00737899243800300, -13.28793577849899066 ) ) ;
#2269=DIRECTION ( 'NONE',  ( 0.000000000000000000, 0.000000000000000000, 1.000000000000000000 ) ) ;
#2275=DIRECTION ( 'NONE',  ( -1.000000000000000000, 0.000000000000000000, 0.000000000000000000 ) ) ;
#2284=AXIS2_PLACEMENT_3D ( 'NONE', #962, #10209, #14882 ) ;
#2285=CARTESIAN_POINT ( 'NONE',  ( -35.81405311550189197, 6.021066563906106950, 29.58511937964010485 ) ) ;
#2286=CARTESIAN_POINT ( 'NONE',  ( -15.49969986081099904, 13.89262100756199736, 18.96206422150099868 ) ) ;
#2298=AXIS2_PLACEMENT_3D ( 'NONE', #8828, #13512, #7682 ) ;
#2301=AXIS2_PLACEMENT_3D ( 'NONE', #13240, #14527, #1322 ) ;
#2307=CARTESIAN_POINT ( 'NONE',  ( -18.72720981345337421, -4.041066102621154954, 61.57426170146454325 ) ) ;
#2312=AXIS2_PLACEMENT_3D ( 'NONE', #7287, #14343, #11732 ) ;
#2316=EDGE_CURVE ( 'NONE', #3863, #12839, #13376, .T. ) ;
#2318=CARTESIAN_POINT ( 'NONE',  ( -28.78282149594069850, -31.14135358865350511, -123.9247733198440073 ) ) ;
#2322=CARTESIAN_POINT ( 'NONE',  ( -11.45509117250411713, -15.50188834333807897, -13.06935246023203234 ) ) ;
#2324=LINE ( 'NONE', #15090, #5063 ) ;
#2329=VERTEX_POINT ( 'NONE', #7740 ) ;
#2334=EDGE_CURVE ( 'NONE', #11422, #6725, #14100, .T. ) ;
#2335=EDGE_CURVE ( 'NONE', #700, #4277, #11126, .T. ) ;
#2336=CARTESIAN_POINT ( 'NONE',  ( 6.045543233663400073, 20.99262100756200056, 32.26206422150099939 ) ) ;
#2339=ORIENTED_EDGE ( 'NONE', *, *, #1951, .T. ) ;
#2353=EDGE_CURVE ( 'NONE', #8123, #11256, #11047, .T. ) ;
#2361=CARTESIAN_POINT ( 'NONE',  ( -31.79969986081099975, 20.99262100756200056, 16.16206422150100153 ) ) ;
#2362=FACE_OUTER_BOUND ( 'NONE', #8921, .T. ) ;
#2371=DIRECTION ( 'NONE',  ( 1.000000000000000000, -3.922012711866029438E-32, 3.202566417187950042E-16 ) ) ;
#2383=VERTEX_POINT ( 'NONE', #7668 ) ;
#2403=EDGE_CURVE ( 'NONE', #12952, #15056, #2324, .T. ) ;
#2413=CARTESIAN_POINT ( 'NONE',  ( -38.28773376859625444, 4.602115691098226158, 27.34154685965552645 ) ) ;
#2419=CARTESIAN_POINT ( 'NONE',  ( 21.93911714261352941, -29.45684053363936883, 26.35858622364352399 ) ) ;
#2424=EDGE_LOOP ( 'NONE', ( #5052, #14852, #3682, #2161 ) ) ;
#2427=LINE ( 'NONE', #7065, #969 ) ;
#2430=LINE ( 'NONE', #3497, #8442 ) ;
#2431=DIRECTION ( 'NONE',  ( 0.000000000000000000, 1.239088197126290817E-16, -1.000000000000000000 ) ) ;
#2434=CARTESIAN_POINT ( 'NONE',  ( -35.74200939090608387, 6.055639158907344388, 29.62312773453597003 ) ) ;
#2446=CARTESIAN_POINT ( 'NONE',  ( -31.79969986081099975, 20.99262100756200056, 32.26206422150099939 ) ) ;
#2448=PLANE ( 'NONE',  #1863 ) ;
#2453=EDGE_CURVE ( 'NONE', #4606, #2975, #5528, .T. ) ;
#2456=DIRECTION ( 'NONE',  ( 1.000000000000000000, 0.000000000000000000, 0.000000000000000000 ) ) ;
#2457=ORIENTED_EDGE ( 'NONE', *, *, #5998, .T. ) ;
#2466=CARTESIAN_POINT ( 'NONE',  ( 18.47619366413413644, -26.09922607948998774, 8.340974680435991218 ) ) ;
#2469=DIRECTION ( 'NONE',  ( -1.000000000000000000, 0.000000000000000000, 0.000000000000000000 ) ) ;
#2476=VECTOR ( 'NONE', #8666, 1000.000000000000000 ) ;
#2478=DIRECTION ( 'NONE',  ( 0.000000000000000000, 0.000000000000000000, 1.000000000000000000 ) ) ;
#2484=EDGE_LOOP ( 'NONE', ( #490, #90 ) ) ;
#2491=CIRCLE ( 'NONE', #9817, 37.50000000000000000 ) ;
#2497=CARTESIAN_POINT ( 'NONE',  ( 7.000300139189000070, -32.00737899243799944, -5.787935778498998651 ) ) ;
#2502=CARTESIAN_POINT ( 'NONE',  ( -15.49969986081099904, -19.50737899243800300, 24.21206422150100224 ) ) ;
#2505=ORIENTED_EDGE ( 'NONE', *, *, #8960, .F. ) ;
#2511=EDGE_LOOP ( 'NONE', ( #13467, #8061, #11179, #554 ) ) ;
#2515=MANIFOLD_SOLID_BREP ( 'Stock-MAS-672-1', #13427 ) ;
#2519=EDGE_CURVE ( 'NONE', #8879, #8329, #7975, .T. ) ;
#2535=AXIS2_PLACEMENT_3D ( 'NONE', #4631, #9204, #10362 ) ;
#2543=CIRCLE ( 'NONE', #6419, 6.828234652215419587 ) ;
#2546=EDGE_LOOP ( 'NONE', ( #8146, #2813 ) ) ;
#2554=B_SPLINE_CURVE_WITH_KNOTS ( 'NONE', 3,
 ( #3175, #4403, #2028, #9978, #6676, #11361, #6954, #13733, #4096, #884, #10205, #9053, #14654, #4174, #11639, #1159, #5820, #8827, #10802, #10571, #11795, #4842, #1469, #8425, #2466, #12878, #8346, #10645 ),
 .UNSPECIFIED., .F., .F.,
 ( 4, 2, 2, 2, 2, 2, 2, 2, 2, 2, 2, 2, 2, 4 ),
 ( 0.01102632501636353554, 0.01171604659087003078, 0.01240576816537652602, 0.01309548973988301952, 0.01378521131438951476, 0.01516465446340249310, 0.01654409761241547316, 0.01792354076142845323, 0.01861326233593494500, 0.01930298391044144024, 0.01999270548494793548, 0.02068242705945443072, 0.02137214863396092943, 0.02206187020846742466 ),
 .UNSPECIFIED. ) ;
#2558=DIRECTION ( 'NONE',  ( -1.000000000000000000, 0.000000000000000000, 0.000000000000000000 ) ) ;
#2560=CARTESIAN_POINT ( 'NONE',  ( -15.49969986081099904, 22.99262100756200056, 24.21206422150099868 ) ) ;
#2564=ORIENTED_EDGE ( 'NONE', *, *, #6404, .F. ) ;
#2569=CARTESIAN_POINT ( 'NONE',  ( 21.85920135429435263, -27.22217168940073506, 27.46206422150099868 ) ) ;
#2571=ORIENTED_EDGE ( 'NONE', *, *, #9640, .T. ) ;
#2580=DIRECTION ( 'NONE',  ( 0.000000000000000000, 0.000000000000000000, 1.000000000000000000 ) ) ;
#2597=CARTESIAN_POINT ( 'NONE',  ( 15.30932787659218697, -29.23053613443893539, 2.832475549366952894 ) ) ;
#2599=CARTESIAN_POINT ( 'NONE',  ( -15.49969986081099904, 7.183219930803499409, 5.212064221501000461 ) ) ;
#2607=EDGE_LOOP ( 'NONE', ( #7484, #665, #2571, #3191 ) ) ;
#2622=AXIS2_PLACEMENT_3D ( 'NONE', #9942, #1765, #14617 ) ;
#2627=ORIENTED_EDGE ( 'NONE', *, *, #1777, .F. ) ;
#2635=CYLINDRICAL_SURFACE ( 'NONE', #2312, 6.250000000000001776 ) ;
#2637=CARTESIAN_POINT ( 'NONE',  ( -38.47046344045732980, 4.067408198524466556, 25.52674954571450172 ) ) ;
#2640=VECTOR ( 'NONE', #1530, 1000.000000000000000 ) ;
#2641=AXIS2_PLACEMENT_3D ( 'NONE', #10036, #499, #8816 ) ;
#2643=VERTEX_POINT ( 'NONE', #9774 ) ;
#2647=ADVANCED_FACE ( 'NONE', ( #10774 ), #4343, .T. ) ;
#2650=CARTESIAN_POINT ( 'NONE',  ( 22.00030013918900096, -27.00737899243800300, 5.212064221501000461 ) ) ;
#2651=ADVANCED_FACE ( 'NONE', ( #7541 ), #1732, .T. ) ;
#2653=CARTESIAN_POINT ( 'NONE',  ( -15.49969986081099904, 12.99262100756199878, 24.21206422150099868 ) ) ;
#2657=CARTESIAN_POINT ( 'NONE',  ( -15.49969986081099904, -19.50737899243800300, 24.21206422150100224 ) ) ;
#2665=CARTESIAN_POINT ( 'NONE',  ( -35.18530787408519700, 11.99262100756819827, 32.26206422150099939 ) ) ;
#2679=CARTESIAN_POINT ( 'NONE',  ( -15.49969986081099904, 12.99262100756199523, 47.21206422150100224 ) ) ;
#2680=VECTOR ( 'NONE', #8033, 1000.000000000000000 ) ;
#2691=CARTESIAN_POINT ( 'NONE',  ( -19.40322886457036589, -11.24908093416351207, -13.08458187592522393 ) ) ;
#2696=CIRCLE ( 'NONE', #12718, 19.00000000000000000 ) ;
#2700=ORIENTED_EDGE ( 'NONE', *, *, #7662, .T. ) ;
#2716=CARTESIAN_POINT ( 'NONE',  ( -25.49893968439952729, -13.50738396921345519, 60.35575980305132049 ) ) ;
#2719=LINE ( 'NONE', #14571, #778 ) ;
#2730=CARTESIAN_POINT ( 'NONE',  ( 0.1306401100565875439, -27.07585217469818772, 58.39162460182395620 ) ) ;
#2740=AXIS2_PLACEMENT_3D ( 'NONE', #14775, #9024, #14922 ) ;
#2742=ADVANCED_FACE ( 'NONE', ( #14546 ), #13478, .T. ) ;
#2747=AXIS2_PLACEMENT_3D ( 'NONE', #12753, #4484, #9139 ) ;
#2755=CARTESIAN_POINT ( 'NONE',  ( 1.891335946368680965, 9.431003388506290719, 31.86906368936717016 ) ) ;
#2756=ORIENTED_EDGE ( 'NONE', *, *, #7653, .T. ) ;
#2764=AXIS2_PLACEMENT_3D ( 'NONE', #11492, #4612, #4462 ) ;
#2765=CARTESIAN_POINT ( 'NONE',  ( -32.80866482175071042, 10.04760564993947192, 16.37540628458954117 ) ) ;
#2784=VECTOR ( 'NONE', #7976, 1000.000000000000000 ) ;
#2785=CARTESIAN_POINT ( 'NONE',  ( -38.49165779676476262, 4.011311318234620948, 23.52756386907951835 ) ) ;
#2787=CARTESIAN_POINT ( 'NONE',  ( -36.01752465275215798, 5.923502402104435127, 18.94969861057483840 ) ) ;
#2790=ORIENTED_EDGE ( 'NONE', *, *, #2178, .T. ) ;
#2791=CARTESIAN_POINT ( 'NONE',  ( -25.45708195274498209, -14.57695636912345272, 60.36601798875501146 ) ) ;
#2794=AXIS2_PLACEMENT_3D ( 'NONE', #6610, #7766, #12755 ) ;
#2799=ADVANCED_FACE ( 'NONE', ( #7574 ), #13698, .F. ) ;
#2800=CARTESIAN_POINT ( 'NONE',  ( 4.899902721674559203, 5.980169784831477209, 18.88473108487603724 ) ) ;
#2805=FACE_OUTER_BOUND ( 'NONE', #8180, .T. ) ;
#2813=ORIENTED_EDGE ( 'NONE', *, *, #12156, .F. ) ;
#2815=ORIENTED_EDGE ( 'NONE', *, *, #6696, .F. ) ;
#2821=FACE_OUTER_BOUND ( 'NONE', #6571, .T. ) ;
#2822=CARTESIAN_POINT ( 'NONE',  ( 7.000300139189000070, -32.00737899243799944, 54.21206422150100224 ) ) ;
#2829=CARTESIAN_POINT ( 'NONE',  ( -15.49969986081099904, 0.9926210075619987805, 24.21206422150099868 ) ) ;
#2833=ORIENTED_EDGE ( 'NONE', *, *, #5507, .F. ) ;
#2843=VECTOR ( 'NONE', #12707, 1000.000000000000000 ) ;
#2844=VERTEX_POINT ( 'NONE', #11250 ) ;
#2865=DIRECTION ( 'NONE',  ( 0.000000000000000000, 1.000000000000000000, 1.224646799147350002E-16 ) ) ;
#2866=ORIENTED_EDGE ( 'NONE', *, *, #12920, .T. ) ;
#2868=CARTESIAN_POINT ( 'NONE',  ( -31.79969986081099975, 3.992621007561997892, 24.21206422150099868 ) ) ;
#2873=DIRECTION ( 'NONE',  ( 0.000000000000000000, 1.224646799147350002E-16, -1.000000000000000000 ) ) ;
#2882=CARTESIAN_POINT ( 'NONE',  ( 21.94831093474578765, -24.42285204022288880, 22.23025988852434409 ) ) ;
#2887=CIRCLE ( 'NONE', #8009, 10.00000000000000000 ) ;
#2889=ADVANCED_FACE ( 'NONE', ( #770 ), #5429, .F. ) ;
#2896=DIRECTION ( 'NONE',  ( 3.632077277826439854E-16, -1.000000000000000000, 0.000000000000000000 ) ) ;
#2904=ORIENTED_EDGE ( 'NONE', *, *, #11484, .T. ) ;
#2906=DIRECTION ( 'NONE',  ( 0.000000000000000000, 0.000000000000000000, -1.000000000000000000 ) ) ;
#2928=DIRECTION ( 'NONE',  ( 0.000000000000000000, 0.000000000000000000, 1.000000000000000000 ) ) ;
#2930=CARTESIAN_POINT ( 'NONE',  ( -11.45455878058586663, -11.51418830146718797, -13.06929284164692540 ) ) ;
#2938=VERTEX_POINT ( 'NONE', #6939 ) ;
#2943=DIRECTION ( 'NONE',  ( -1.000000000000000000, 0.000000000000000000, 0.000000000000000000 ) ) ;
#2947=ADVANCED_FACE ( 'NONE', ( #8249 ), #2448, .T. ) ;
#2948=CARTESIAN_POINT ( 'NONE',  ( 4.903189148188024760, 5.978594350615844988, 18.88651708455363476 ) ) ;
#2950=DIRECTION ( 'NONE',  ( 1.000000000000000000, 0.000000000000000000, 1.224646799147350002E-16 ) ) ;
#2954=DIRECTION ( 'NONE',  ( 1.000000000000000000, 0.000000000000000000, 0.000000000000000000 ) ) ;
#2958=ORIENTED_EDGE ( 'NONE', *, *, #7054, .T. ) ;
#2962=DIRECTION ( 'NONE',  ( 0.000000000000000000, 1.000000000000000000, 1.224646799147350002E-16 ) ) ;
#2971=ORIENTED_EDGE ( 'NONE', *, *, #12281, .F. ) ;
#2972=EDGE_CURVE ( 'NONE', #5899, #13245, #10324, .T. ) ;
#2975=VERTEX_POINT ( 'NONE', #4520 ) ;
#2981=EDGE_CURVE ( 'NONE', #9211, #6978, #3366, .T. ) ;
#2984=TOROIDAL_SURFACE ( 'NONE', #12775, 28.00000000000000000, 5.000000000000000000 ) ;
#2992=LINE ( 'NONE', #14401, #14463 ) ;
#3001=VERTEX_POINT ( 'NONE', #4974 ) ;
#3004=EDGE_CURVE ( 'NONE', #13270, #2938, #14507, .T. ) ;
#3005=FACE_OUTER_BOUND ( 'NONE', #7966, .T. ) ;
#3006=AXIS2_PLACEMENT_3D ( 'NONE', #3820, #9639, #164 ) ;
#3021=DIRECTION ( 'NONE',  ( 8.659560562354914369E-17, 0.7071067811865491270, -0.7071067811865459074 ) ) ;
#3027=EDGE_CURVE ( 'NONE', #8801, #15009, #5046, .T. ) ;
#3028=EDGE_LOOP ( 'NONE', ( #9186, #4956, #1131, #2833 ) ) ;
#3035=ORIENTED_EDGE ( 'NONE', *, *, #8093, .T. ) ;
#3047=EDGE_CURVE ( 'NONE', #8556, #14647, #6246, .T. ) ;
#3048=ORIENTED_EDGE ( 'NONE', *, *, #181, .F. ) ;
#3050=VERTEX_POINT ( 'NONE', #2822 ) ;
#3058=CARTESIAN_POINT ( 'NONE',  ( -38.49895354373176559, 3.992621007561999669, 23.84375914672395780 ) ) ;
#3074=FACE_OUTER_BOUND ( 'NONE', #7797, .T. ) ;
#3082=CARTESIAN_POINT ( 'NONE',  ( -38.49964551292070070, 3.992621007561997892, 24.26206422150100650 ) ) ;
#3093=DIRECTION ( 'NONE',  ( 9.263529044864487894E-17, -0.6540809579092763393, 0.7564245504347960614 ) ) ;
#3099=CARTESIAN_POINT ( 'NONE',  ( 5.121633317442411126, 5.873878172623350657, 29.41645846257583941 ) ) ;
#3101=DIRECTION ( 'NONE',  ( 0.000000000000000000, 1.000000000000000000, 1.224646799147350002E-16 ) ) ;
#3106=CARTESIAN_POINT ( 'NONE',  ( 21.96528430198313941, -24.18757308759200342, 22.58233337257930984 ) ) ;
#3110=CARTESIAN_POINT ( 'NONE',  ( -15.49969986081099904, 64.39262100756199914, 24.21206422150100579 ) ) ;
#3112=CARTESIAN_POINT ( 'NONE',  ( -31.89126067837590028, -25.75737899243799944, -123.9247733198440073 ) ) ;
#3117=CIRCLE ( 'NONE', #13865, 37.50000000000000000 ) ;
#3120=ORIENTED_EDGE ( 'NONE', *, *, #12366, .F. ) ;
#3122=( BOUNDED_CURVE ( )  B_SPLINE_CURVE ( 3, ( #12708, #4596, #14001, #4826 ),
 .UNSPECIFIED., .F., .T. ) 
 B_SPLINE_CURVE_WITH_KNOTS ( ( 4, 4 ),
 ( 1.008260082251041245, 1.208720131788790120 ),
 .UNSPECIFIED. ) 
 CURVE ( )  GEOMETRIC_REPRESENTATION_ITEM ( )  RATIONAL_B_SPLINE_CURVE ( ( 1.000000000000000000, 0.9966541165307394312, 0.9966541165307394312, 1.000000000000000000 ) ) 
 REPRESENTATION_ITEM ( '' )  );
#3139=CIRCLE ( 'NONE', #9383, 5.250000000000000888 ) ;
#3142=ORIENTED_EDGE ( 'NONE', *, *, #13101, .F. ) ;
#3143=CARTESIAN_POINT ( 'NONE',  ( 17.56443294355201346, -29.99028402068969257, 41.90559943672241872 ) ) ;
#3149=FACE_OUTER_BOUND ( 'NONE', #11782, .T. ) ;
#3162=VERTEX_POINT ( 'NONE', #6619 ) ;
#3166=CARTESIAN_POINT ( 'NONE',  ( -15.49969986081099904, 2.992621007561997004, 24.21206422150099868 ) ) ;
#3167=DIRECTION ( 'NONE',  ( 0.000000000000000000, -1.225619847157526848E-16, 1.000000000000000000 ) ) ;
#3168=EDGE_LOOP ( 'NONE', ( #1715, #11575, #11441, #14757 ) ) ;
#3169=B_SPLINE_CURVE_WITH_KNOTS ( 'NONE', 3,
 ( #7974, #13954, #882, #13658 ),
 .UNSPECIFIED., .F., .F.,
 ( 4, 4 ),
 ( 0.000000000000000000, 1.000000000000000000 ),
 .UNSPECIFIED. ) ;
#3175=CARTESIAN_POINT ( 'NONE',  ( 14.68618260102866913, -27.00737899243800300, 1.962064221501000683 ) ) ;
#3180=ORIENTED_EDGE ( 'NONE', *, *, #4898, .T. ) ;
#3191=ORIENTED_EDGE ( 'NONE', *, *, #11751, .F. ) ;
#3194=ADVANCED_FACE ( 'NONE', ( #12534 ), #12460, .F. ) ;
#3200=CARTESIAN_POINT ( 'NONE',  ( -19.99969986081099904, -13.50737899243800122, -13.01695671647154917 ) ) ;
#3212=CARTESIAN_POINT ( 'NONE',  ( -6.840406258826835284, -8.492485342089160838, 60.69893026050551299 ) ) ;
#3216=CARTESIAN_POINT ( 'NONE',  ( -38.49964551292070070, 3.992621007561997892, 24.16206422150099442 ) ) ;
#3219=CARTESIAN_POINT ( 'NONE',  ( 18.35491122210689596, -28.54603682261319619, 40.34048003543883709 ) ) ;
#3222=CARTESIAN_POINT ( 'NONE',  ( -25.49893968439952729, -13.50738396921345519, 60.35575980305132049 ) ) ;
#3227=VECTOR ( 'NONE', #15093, 1000.000000000000000 ) ;
#3234=( NAMED_UNIT ( * ) SI_UNIT ( $, .STERADIAN. ) SOLID_ANGLE_UNIT ( ) );
#3237=VERTEX_POINT ( 'NONE', #11080 ) ;
#3239=AXIS2_PLACEMENT_3D ( 'NONE', #13741, #2192, #2269 ) ;
#3247=B_SPLINE_CURVE_WITH_KNOTS ( 'NONE', 3,
 ( #11478, #12404, #11180, #11401, #1924, #5363, #10019, #4373, #929, #11254, #6795, #14848, #4444, #13556, #9100, #5656, #7947, #13628, #774, #14694, #13852, #3143, #7795, #12481, #5509, #5581, #1002, #1996, #3219, #13781, #10328, #3299, #2153, #9173 ),
 .UNSPECIFIED., .F., .F.,
 ( 4, 2, 2, 2, 2, 2, 2, 2, 2, 2, 2, 2, 2, 2, 2, 2, 4 ),
 ( 0.000000000000000000, 0.0006890873081066433998, 0.001378174616213286800, 0.002067261924319929983, 0.002756349232426573599, 0.003445436540533216782, 0.004134523848639857363, 0.004823611156746498811, 0.005512698464853139392, 0.006201785772959779973, 0.006890873081066421421, 0.007579960389173062002, 0.008269047697279702583, 0.008958135005386344898, 0.009647222313492983745, 0.01033630962159962606, 0.01102539692970626664 ),
 .UNSPECIFIED. ) ;
#3248=ORIENTED_EDGE ( 'NONE', *, *, #650, .T. ) ;
#3264=ORIENTED_EDGE ( 'NONE', *, *, #13201, .F. ) ;
#3274=VECTOR ( 'NONE', #5627, 1000.000000000000000 ) ;
#3283=EDGE_CURVE ( 'NONE', #9649, #1266, #11678, .T. ) ;
#3289=DIRECTION ( 'NONE',  ( -1.000000000000000000, 0.000000000000000000, 0.000000000000000000 ) ) ;
#3294=VECTOR ( 'NONE', #5354, 1000.000000000000000 ) ;
#3299=CARTESIAN_POINT ( 'NONE',  ( 18.52131844622569190, -27.46537016822669841, 39.98619483191109225 ) ) ;
#3303=CARTESIAN_POINT ( 'NONE',  ( -23.82607259144200285, -7.937054303016555679, 60.77739987434360813 ) ) ;
#3315=CARTESIAN_POINT ( 'NONE',  ( 14.95712091018315704, -25.48139565519610983, 46.09000694556162614 ) ) ;
#3316=ORIENTED_EDGE ( 'NONE', *, *, #8016, .T. ) ;
#3321=ORIENTED_EDGE ( 'NONE', *, *, #2981, .T. ) ;
#3329=CARTESIAN_POINT ( 'NONE',  ( 4.920768659932027056, 5.970170166553373292, 29.52801776241059883 ) ) ;
#3334=ORIENTED_EDGE ( 'NONE', *, *, #10184, .T. ) ;
#3352=DIRECTION ( 'NONE',  ( 0.000000000000000000, 1.000000000000000000, 1.224646799147350002E-16 ) ) ;
#3353=ORIENTED_EDGE ( 'NONE', *, *, #10501, .T. ) ;
#3354=DIRECTION ( 'NONE',  ( 0.000000000000000000, 0.000000000000000000, 1.000000000000000000 ) ) ;
#3355=ORIENTED_EDGE ( 'NONE', *, *, #1777, .T. ) ;
#3357=CARTESIAN_POINT ( 'NONE',  ( 0.8003001391889992266, 20.99262100756200056, 32.26206422150099939 ) ) ;
#3364=CARTESIAN_POINT ( 'NONE',  ( -5.586161854270613958, -12.19953394658199386, 60.37797296075051889 ) ) ;
#3366=LINE ( 'NONE', #7012, #2843 ) ;
#3370=CARTESIAN_POINT ( 'NONE',  ( 13.85920135429429934, -27.00737899243800300, 27.46206422150099868 ) ) ;
#3378=ADVANCED_FACE ( 'NONE', ( #10382 ), #11455, .F. ) ;
#3382=CARTESIAN_POINT ( 'NONE',  ( -37.04494295528539993, 0.9926210075619987805, 32.26206422150099939 ) ) ;
#3385=EDGE_CURVE ( 'NONE', #9045, #8329, #2430, .T. ) ;
#3390=CARTESIAN_POINT ( 'NONE',  ( -2.216578225681298697, -32.00737899243799944, -10.85656391856669778 ) ) ;
#3392=CARTESIAN_POINT ( 'NONE',  ( -10.99969986081099904, -13.50737899243800122, -13.01695671647155983 ) ) ;
#3395=ORIENTED_EDGE ( 'NONE', *, *, #6434, .T. ) ;
#3403=DIRECTION ( 'NONE',  ( 0.000000000000000000, 0.000000000000000000, 1.000000000000000000 ) ) ;
#3405=CARTESIAN_POINT ( 'NONE',  ( 3.107080982810261460, 6.836425395121002779, 30.39410943549851751 ) ) ;
#3419=CARTESIAN_POINT ( 'NONE',  ( 22.00030013918900096, -27.00737899243800300, 2.712064221501000461 ) ) ;
#3422=CARTESIAN_POINT ( 'NONE',  ( -15.49969986081099371, -18.00737899243799944, -13.28793577849899776 ) ) ;
#3425=CARTESIAN_POINT ( 'NONE',  ( 22.00030013918900096, -27.00737899243800300, 5.212064221501000461 ) ) ;
#3429=VERTEX_POINT ( 'NONE', #9458 ) ;
#3436=LINE ( 'NONE', #2446, #11771 ) ;
#3442=ORIENTED_EDGE ( 'NONE', *, *, #10501, .F. ) ;
#3446=CARTESIAN_POINT ( 'NONE',  ( -20.51036999038052144, -4.847632558696703953, 61.37692998373628228 ) ) ;
#3447=VERTEX_POINT ( 'NONE', #2497 ) ;
#3450=CYLINDRICAL_SURFACE ( 'NONE', #14121, 22.99999999999999645 ) ;
#3453=EDGE_CURVE ( 'NONE', #1539, #8623, #14072, .T. ) ;
#3462=ORIENTED_EDGE ( 'NONE', *, *, #980, .T. ) ;
#3467=ADVANCED_FACE ( 'NONE', ( #7384 ), #13146, .F. ) ;
#3482=CYLINDRICAL_SURFACE ( 'NONE', #10342, 8.000000000000000000 ) ;
#3483=ORIENTED_EDGE ( 'NONE', *, *, #10090, .T. ) ;
#3493=CARTESIAN_POINT ( 'NONE',  ( 9.000300139189000959, -19.50737899243799589, -4.178074911655800250 ) ) ;
#3495=ADVANCED_FACE ( 'NONE', ( #2805, #7457 ), #5931, .T. ) ;
#3497=CARTESIAN_POINT ( 'NONE',  ( -5.499699860810999041, -19.50737899243799589, 6.712064221500998684 ) ) ;
#3502=CARTESIAN_POINT ( 'NONE',  ( -35.87823185118522673, 5.990273379230379724, 29.55080429321562363 ) ) ;
#3513=CARTESIAN_POINT ( 'NONE',  ( -5.500158185064795369, -14.04218574468902148, 60.35427179981845569 ) ) ;
#3523=ORIENTED_EDGE ( 'NONE', *, *, #14196, .F. ) ;
#3524=CARTESIAN_POINT ( 'NONE',  ( -25.40982920130948841, -12.19918686643515038, 60.37889978234523625 ) ) ;
#3531=DIRECTION ( 'NONE',  ( 0.000000000000000000, 0.000000000000000000, -1.000000000000000000 ) ) ;
#3542=VERTEX_POINT ( 'NONE', #12242 ) ;
#3543=DIRECTION ( 'NONE',  ( 0.000000000000000000, 1.000000000000000000, 1.224646799147350002E-16 ) ) ;
#3544=ORIENTED_EDGE ( 'NONE', *, *, #1222, .F. ) ;
#3546=CARTESIAN_POINT ( 'NONE',  ( 0.8003001391889992266, 11.99262100756199878, 16.16206422150100153 ) ) ;
#3551=DIRECTION ( 'NONE',  ( 0.000000000000000000, 9.130123557772668334E-17, -1.000000000000000000 ) ) ;
#3563=CARTESIAN_POINT ( 'NONE',  ( 21.92071449028411934, -29.15732165064080661, 26.65852393176527713 ) ) ;
#3567=VERTEX_POINT ( 'NONE', #4130 ) ;
#3572=DIRECTION ( 'NONE',  ( -1.000000000000000000, 3.922012711866029438E-32, -3.202566417187950042E-16 ) ) ;
#3577=CARTESIAN_POINT ( 'NONE',  ( -35.90258886980872433, 5.978594350616473818, 29.53761135844903052 ) ) ;
#3582=EDGE_LOOP ( 'NONE', ( #14028, #2505, #15092, #11861, #4506 ) ) ;
#3608=DIRECTION ( 'NONE',  ( 0.000000000000000000, 9.130123557772668334E-17, -1.000000000000000000 ) ) ;
#3612=CARTESIAN_POINT ( 'NONE',  ( -19.54288648179596422, -11.51027871586804352, -13.06950530299294577 ) ) ;
#3621=EDGE_LOOP ( 'NONE', ( #9381, #14454, #10489 ) ) ;
#3629=CIRCLE ( 'NONE', #7028, 23.00000000000000000 ) ;
#3637=DIRECTION ( 'NONE',  ( 0.000000000000000000, 1.000000000000000000, 1.224646799147350002E-16 ) ) ;
#3640=CARTESIAN_POINT ( 'NONE',  ( 21.93891671199435223, -29.45378376108857310, 22.06206851614466302 ) ) ;
#3649=CARTESIAN_POINT ( 'NONE',  ( 7.292741504061227786, 4.584400082011329758, 27.34761902326144423 ) ) ;
#3651=AXIS2_PLACEMENT_3D ( 'NONE', #14061, #9694, #10773 ) ;
#3658=CARTESIAN_POINT ( 'NONE',  ( -35.89930244329396913, 5.980169784832726876, 29.53939735812734568 ) ) ;
#3666=EDGE_CURVE ( 'NONE', #1380, #12994, #5909, .T. ) ;
#3670=DIRECTION ( 'NONE',  ( 0.000000000000000000, -1.850371707708594316E-16, 1.000000000000000000 ) ) ;
#3672=CARTESIAN_POINT ( 'NONE',  ( 14.68618260102866913, -27.00737899243800300, 1.962064221501000683 ) ) ;
#3673=EDGE_LOOP ( 'NONE', ( #10733, #9029, #12502, #6170 ) ) ;
#3678=CARTESIAN_POINT ( 'NONE',  ( 7.392926877888857717, 4.291769771411865442, 21.97069516755205498 ) ) ;
#3682=ORIENTED_EDGE ( 'NONE', *, *, #3453, .F. ) ;
#3687=DIRECTION ( 'NONE',  ( 3.632077277826439854E-16, -1.000000000000000000, 0.000000000000000000 ) ) ;
#3688=LINE ( 'NONE', #4917, #12727 ) ;
#3695=DIRECTION ( 'NONE',  ( 1.000000000000000000, 0.000000000000000000, 0.000000000000000000 ) ) ;
#3709=DIRECTION ( 'NONE',  ( 0.000000000000000000, 1.000000000000000000, 1.224646799147350002E-16 ) ) ;
#3713=ORIENTED_EDGE ( 'NONE', *, *, #7358, .T. ) ;
#3715=CARTESIAN_POINT ( 'NONE',  ( 21.86822340939376019, -27.85492751190550109, 27.35691555891743221 ) ) ;
#3721=AXIS2_PLACEMENT_3D ( 'NONE', #13676, #6615, #6394 ) ;
#3728=DIRECTION ( 'NONE',  ( 1.000000000000000000, 3.700743415417188632E-16, 0.000000000000000000 ) ) ;
#3731=EDGE_LOOP ( 'NONE', ( #13094, #1257, #15047, #12883 ) ) ;
#3734=FACE_OUTER_BOUND ( 'NONE', #4223, .T. ) ;
#3738=DIRECTION ( 'NONE',  ( 0.000000000000000000, 1.224646799147350002E-16, -1.000000000000000000 ) ) ;
#3741=CARTESIAN_POINT ( 'NONE',  ( -35.80601265084419538, 12.32432269366989530, 16.16206422150100153 ) ) ;
#3742=CARTESIAN_POINT ( 'NONE',  ( -15.49969986081099904, 20.99262100756200056, 24.21206422150099868 ) ) ;
#3743=AXIS2_PLACEMENT_3D ( 'NONE', #14080, #12017, #11781 ) ;
#3745=CARTESIAN_POINT ( 'NONE',  ( 17.35862657855726354, -30.12898149287163108, 6.139218436208705221 ) ) ;
#3749=EDGE_CURVE ( 'NONE', #7451, #14647, #4458, .T. ) ;
#3760=AXIS2_PLACEMENT_3D ( 'NONE', #13906, #1202, #2431 ) ;
#3762=LINE ( 'NONE', #8418, #1934 ) ;
#3763=CARTESIAN_POINT ( 'NONE',  ( -35.18530787408279537, 11.99262100756689620, 16.16206422150100153 ) ) ;
#3772=( NAMED_UNIT ( * ) PLANE_ANGLE_UNIT ( ) SI_UNIT ( $, .RADIAN. ) );
#3782=CYLINDRICAL_SURFACE ( 'NONE', #10964, 2.500000000000002220 ) ;
#3786=CARTESIAN_POINT ( 'NONE',  ( -38.20013690429809827, 4.873818854045000037, 27.91208557747711083 ) ) ;
#3792=CARTESIAN_POINT ( 'NONE',  ( 21.91137017292814093, -28.99035275200779083, 21.62826645491238509 ) ) ;
#3799=CARTESIAN_POINT ( 'NONE',  ( -15.49969986081099904, 7.183219930803497633, 24.21206422150099868 ) ) ;
#3810=DIRECTION ( 'NONE',  ( 0.000000000000000000, -1.508455196501571676E-16, 1.000000000000000000 ) ) ;
#3813=DIRECTION ( 'NONE',  ( 0.000000000000000000, 1.000000000000000000, 1.224646799147350002E-16 ) ) ;
#3820=CARTESIAN_POINT ( 'NONE',  ( -15.49969986081099904, 2.992621007561997004, 24.21206422150099868 ) ) ;
#3825=ORIENTED_EDGE ( 'NONE', *, *, #2453, .F. ) ;
#3833=VECTOR ( 'NONE', #2244, 1000.000000000000000 ) ;
#3836=CARTESIAN_POINT ( 'NONE',  ( -15.79707957972810384, -9.007378992438001220, -13.28793577849899599 ) ) ;
#3841=ORIENTED_EDGE ( 'NONE', *, *, #6744, .T. ) ;
#3842=CARTESIAN_POINT ( 'NONE',  ( -15.49969986081099904, 70.81438635534659909, 24.21206422150100579 ) ) ;
#3862=ORIENTED_EDGE ( 'NONE', *, *, #8128, .F. ) ;
#3863=VERTEX_POINT ( 'NONE', #13004 ) ;
#3864=CARTESIAN_POINT ( 'NONE',  ( 21.97302893587540851, -29.92705860424354825, 22.76870634099842761 ) ) ;
#3867=CIRCLE ( 'NONE', #6531, 8.886381701226328644 ) ;
#3872=B_SPLINE_CURVE_WITH_KNOTS ( 'NONE', 3,
 ( #7453, #6594, #13509, #9976, #6451, #5164, #12287, #12358, #582, #4171, #12130, #2800, #2948, #14651, #8751, #1647, #10044, #9837, #11059 ),
 .UNSPECIFIED., .F., .F.,
 ( 4, 2, 2, 2, 1, 1, 1, 1, 1, 2, 2, 4 ),
 ( 0.000000000000000000, 0.2500000000000998090, 0.3750000000001501577, 0.4375000000001756373, 0.4687500000001887379, 0.4843750000001955658, 0.4921875000001992295, 0.4960937500002022826, 0.4980468750002025602, 0.4990234375002016720, 0.5000000000002008393, 1.000000000000000000 ),
 .UNSPECIFIED. ) ;
#3879=CYLINDRICAL_SURFACE ( 'NONE', #11413, 8.000000000000003553 ) ;
#3891=CARTESIAN_POINT ( 'NONE',  ( 22.00030013918900096, -27.00737899243800300, 1.962064221501000683 ) ) ;
#3895=CARTESIAN_POINT ( 'NONE',  ( 17.85498670612308914, -29.68038497774185558, 7.072740731940803549 ) ) ;
#3913=SHAPE_DEFINITION_REPRESENTATION ( #13378, #6151 ) ;
#3929=DIRECTION ( 'NONE',  ( 0.000000000000000000, 1.000000000000000000, 1.224646799147350002E-16 ) ) ;
#3934=CARTESIAN_POINT ( 'NONE',  ( -36.49062000465940514, 5.696595093598766368, 19.22546363248600088 ) ) ;
#3935=ADVANCED_FACE ( 'NONE', ( #11845, #9468 ), #5944, .T. ) ;
#3937=DIRECTION ( 'NONE',  ( 3.202566417187950042E-16, 1.224646799147350002E-16, -1.000000000000000000 ) ) ;
#3939=ORIENTED_EDGE ( 'NONE', *, *, #12976, .T. ) ;
#3940=CARTESIAN_POINT ( 'NONE',  ( -25.15786752016616035, -16.15135352813856073, 60.44742509602125580 ) ) ;
#3954=EDGE_LOOP ( 'NONE', ( #7614, #10618, #13800, #1479 ) ) ;
#3965=CARTESIAN_POINT ( 'NONE',  ( -15.49969986081099904, -2.007378992438000331, 24.21206422150100224 ) ) ;
#3972=CARTESIAN_POINT ( 'NONE',  ( 14.95806614058027861, -28.53604795622425527, 2.335433060012842343 ) ) ;
#3979=CYLINDRICAL_SURFACE ( 'NONE', #13529, 22.99999999999999645 ) ;
#3987=CARTESIAN_POINT ( 'NONE',  ( -13.22804965902115093, -3.767132336032069428, 61.64459019995985756 ) ) ;
#3991=CARTESIAN_POINT ( 'NONE',  ( -15.49969986081099904, 1010.738102757665615, 1688.491546572001198 ) ) ;
#3999=CARTESIAN_POINT ( 'NONE',  ( -15.49969986081099549, 2.992621007561994340, 47.21206422150099513 ) ) ;
#4000=EDGE_LOOP ( 'NONE', ( #6740, #14277 ) ) ;
#4001=CARTESIAN_POINT ( 'NONE',  ( -11.14367517063017310, -12.33997039914164517, -13.03412254519544433 ) ) ;
#4004=CARTESIAN_POINT ( 'NONE',  ( -31.79969986081099975, 20.99262100756200056, 16.16206422150100153 ) ) ;
#4005=DIRECTION ( 'NONE',  ( 1.000000000000000000, 0.000000000000000000, 0.000000000000000000 ) ) ;
#4006=ADVANCED_FACE ( 'NONE', ( #11207 ), #14573, .T. ) ;
#4010=CARTESIAN_POINT ( 'NONE',  ( -35.93898377820745083, 5.961151497827927415, 18.90639720243849098 ) ) ;
#4020=CARTESIAN_POINT ( 'NONE',  ( -15.49969986081099904, -2.007378992438000331, 24.21206422150100579 ) ) ;
#4024=DIRECTION ( 'NONE',  ( 0.000000000000000000, 0.7071067811865489050, 0.7071067811865462405 ) ) ;
#4028=CARTESIAN_POINT ( 'NONE',  ( 2.436724872741607317, 11.05255549926114078, 32.21545598377514352 ) ) ;
#4029=PLANE ( 'NONE',  #9874 ) ;
#4035=B_SPLINE_CURVE_WITH_KNOTS ( 'NONE', 3,
 ( #9402, #3513, #12787, #4900, #4742, #6019, #13010, #7087, #1294, #10703, #11619, #14070 ),
 .UNSPECIFIED., .F., .F.,
 ( 4, 2, 2, 2, 2, 4 ),
 ( 0.8546984898013801901, 0.8910238673510351148, 0.9273492449006901506, 0.9455119336755175574, 0.9636746224503449643, 1.000000000000000000 ),
 .UNSPECIFIED. ) ;
#4036=CARTESIAN_POINT ( 'NONE',  ( 21.92064319118239624, -24.85867307568577544, 26.65960893809553056 ) ) ;
#4040=DIRECTION ( 'NONE',  ( 0.000000000000000000, 1.000000000000000000, 1.224646799147350002E-16 ) ) ;
#4042=DIRECTION ( 'NONE',  ( -1.000000000000000000, 0.000000000000000000, 0.000000000000000000 ) ) ;
#4053=ORIENTED_EDGE ( 'NONE', *, *, #4108, .F. ) ;
#4064=ORIENTED_EDGE ( 'NONE', *, *, #8490, .T. ) ;
#4070=EDGE_CURVE ( 'NONE', #15056, #12659, #2009, .T. ) ;
#4073=CARTESIAN_POINT ( 'NONE',  ( -15.20204784330336878, -9.007378992438004772, -13.28793577849899599 ) ) ;
#4078=DIRECTION ( 'NONE',  ( 0.000000000000000000, 0.000000000000000000, -1.000000000000000000 ) ) ;
#4080=ORIENTED_EDGE ( 'NONE', *, *, #15002, .T. ) ;
#4083=ORIENTED_EDGE ( 'NONE', *, *, #8093, .F. ) ;
#4094=CARTESIAN_POINT ( 'NONE',  ( 9.000300139189000959, -27.00737899243800300, 45.71206422150100224 ) ) ;
#4096=CARTESIAN_POINT ( 'NONE',  ( 15.30745245775401564, -24.78701188282911261, 2.829765091595426441 ) ) ;
#4099=LINE ( 'NONE', #1883, #1327 ) ;
#4108=EDGE_CURVE ( 'NONE', #4618, #8578, #8904, .T. ) ;
#4130=CARTESIAN_POINT ( 'NONE',  ( 4.500300139189000959, -19.50737899243801010, -7.509379629622798369 ) ) ;
#4131=ORIENTED_EDGE ( 'NONE', *, *, #4388, .T. ) ;
#4136=DIRECTION ( 'NONE',  ( 0.000000000000000000, 0.000000000000000000, 1.000000000000000000 ) ) ;
#4140=AXIS2_PLACEMENT_3D ( 'NONE', #2233, #11565, #5745 ) ;
#4144=LINE ( 'NONE', #14549, #1268 ) ;
#4148=ORIENTED_EDGE ( 'NONE', *, *, #388, .F. ) ;
#4150=DIRECTION ( 'NONE',  ( 0.000000000000000000, 1.850371707708594316E-16, -1.000000000000000000 ) ) ;
#4153=CARTESIAN_POINT ( 'NONE',  ( -11.59433051269579806, -11.25225515987115266, -13.08438853397158219 ) ) ;
#4168=ORIENTED_EDGE ( 'NONE', *, *, #723, .T. ) ;
#4171=CARTESIAN_POINT ( 'NONE',  ( 4.878832129573360987, 5.990273379225493855, 18.87332414979169570 ) ) ;
#4174=CARTESIAN_POINT ( 'NONE',  ( 17.02395575395021154, -23.74935330727123173, 5.539182377213959008 ) ) ;
#4178=CARTESIAN_POINT ( 'NONE',  ( -15.49969986081099904, 22.99262100756200056, 24.21206422150100224 ) ) ;
#4179=CARTESIAN_POINT ( 'NONE',  ( 22.00030013918900096, -27.00737899243800300, 46.46206422150100224 ) ) ;
#4180=EDGE_LOOP ( 'NONE', ( #10941, #10905, #10554, #4080, #9864, #3264 ) ) ;
#4181=CARTESIAN_POINT ( 'NONE',  ( 2.304527317575351564, 7.441414002149848272, 30.84924175176620764 ) ) ;
#4182=CARTESIAN_POINT ( 'NONE',  ( 21.99845600427570247, -23.77846206701320142, 23.78571393264229883 ) ) ;
#4184=VERTEX_POINT ( 'NONE', #2251 ) ;
#4188=B_SPLINE_CURVE_WITH_KNOTS ( 'NONE', 3,
 ( #6473, #6552, #14601, #11005, #13319, #12309, #1828, #6329, #13609, #11157, #7777, #11237 ),
 .UNSPECIFIED., .F., .F.,
 ( 4, 2, 2, 2, 2, 4 ),
 ( 0.000000000000000000, 0.2499999999999938938, 0.3749999999999918399, 0.4374999999999926725, 0.4999999999999935607, 1.000000000000000000 ),
 .UNSPECIFIED. ) ;
#4204=ORIENTED_EDGE ( 'NONE', *, *, #7924, .T. ) ;
#4205=DIRECTION ( 'NONE',  ( 1.000000000000000000, -3.922012711866029438E-32, 3.202566417187950042E-16 ) ) ;
#4212=AXIS2_PLACEMENT_3D ( 'NONE', #8321, #3813, #12006 ) ;
#4223=EDGE_LOOP ( 'NONE', ( #14389, #6366 ) ) ;
#4224=ORIENTED_EDGE ( 'NONE', *, *, #13794, .F. ) ;
#4226=CIRCLE ( 'NONE', #11549, 15.62500000000000355 ) ;
#4228=CARTESIAN_POINT ( 'NONE',  ( 1.973171000691426702, 8.982922429311637202, 16.74883253750077117 ) ) ;
#4244=DIRECTION ( 'NONE',  ( 0.000000000000000000, 1.272130549049658454E-16, -1.000000000000000000 ) ) ;
#4246=AXIS2_PLACEMENT_3D ( 'NONE', #6629, #6705, #14830 ) ;
#4248=DIRECTION ( 'NONE',  ( 0.000000000000000000, 0.000000000000000000, 1.000000000000000000 ) ) ;
#4250=CARTESIAN_POINT ( 'NONE',  ( -31.79969986081099975, 20.99262100756200056, 32.26206422150099939 ) ) ;
#4258=EDGE_LOOP ( 'NONE', ( #4652, #11623, #3316, #5239 ) ) ;
#4274=VECTOR ( 'NONE', #1290, 1000.000000000000000 ) ;
#4277=VERTEX_POINT ( 'NONE', #10737 ) ;
#4288=LINE ( 'NONE', #11325, #13548 ) ;
#4300=CARTESIAN_POINT ( 'NONE',  ( -15.49969986081099904, 10.68321993080349586, 43.21206422150100224 ) ) ;
#4303=DIRECTION ( 'NONE',  ( 0.000000000000000000, -1.000000000000000000, -1.224646799147350002E-16 ) ) ;
#4304=ADVANCED_FACE ( 'NONE', ( #10583 ), #7125, .F. ) ;
#4306=EDGE_CURVE ( 'NONE', #4377, #13245, #5923, .T. ) ;
#4314=ORIENTED_EDGE ( 'NONE', *, *, #10377, .T. ) ;
#4330=DIRECTION ( 'NONE',  ( -1.000000000000000000, 1.927249326158850112E-15, -7.070501591499349439E-17 ) ) ;
#4331=CARTESIAN_POINT ( 'NONE',  ( 4.913689842097131333, 5.973563155936592040, 29.53187956306727457 ) ) ;
#4333=CARTESIAN_POINT ( 'NONE',  ( -5.500669204425239656, -13.50739036851649466, 60.35526053768147392 ) ) ;
#4343=CONICAL_SURFACE ( 'NONE', #12896, 23.00000000000000000, 1.047197551196598297 ) ;
#4345=CARTESIAN_POINT ( 'NONE',  ( 7.000300139189000070, -32.00737899243799944, 54.21206422150100224 ) ) ;
#4350=ADVANCED_FACE ( 'NONE', ( #14261 ), #14337, .F. ) ;
#4353=EDGE_LOOP ( 'NONE', ( #8213, #1672, #7039, #389 ) ) ;
#4354=DIRECTION ( 'NONE',  ( -1.000000000000000000, 0.000000000000000000, 0.000000000000000000 ) ) ;
#4358=CARTESIAN_POINT ( 'NONE',  ( 14.68618260102869932, -27.00737899243800300, 46.46206422150099513 ) ) ;
#4360=B_SPLINE_CURVE_WITH_KNOTS ( 'NONE', 3,
 ( #3392, #8042, #6118, #13112, #12964, #2322, #9503, #1324, #9272, #12882, #14097, #1473, #15088, #5825, #13943, #109, #8118, #11644 ),
 .UNSPECIFIED., .F., .F.,
 ( 4, 2, 2, 2, 2, 2, 2, 2, 4 ),
 ( 0.01418968994342788455, 0.01507654967364544137, 0.01596340940386299992, 0.01685026913408055674, 0.01773712886429811356, 0.01862398859451567384, 0.01951084832473323066, 0.02039770805495078748, 0.02128456778516834430 ),
 .UNSPECIFIED. ) ;
#4361=ORIENTED_EDGE ( 'NONE', *, *, #12913, .T. ) ;
#4363=DIRECTION ( 'NONE',  ( -1.000000000000000000, 0.000000000000000000, 0.000000000000000000 ) ) ;
#4373=CARTESIAN_POINT ( 'NONE',  ( 15.21157213869945934, -29.07137141679140768, 45.73161216243208571 ) ) ;
#4377=VERTEX_POINT ( 'NONE', #12113 ) ;
#4381=CARTESIAN_POINT ( 'NONE',  ( 0.000000000000000000, 0.000000000000000000, 0.000000000000000000 ) ) ;
#4382=CIRCLE ( 'NONE', #3651, 8.314203600725839749 ) ;
#4385=EDGE_LOOP ( 'NONE', ( #12143, #3120, #13265, #2627 ) ) ;
#4388=EDGE_CURVE ( 'NONE', #12952, #12465, #12475, .T. ) ;
#4390=CARTESIAN_POINT ( 'NONE',  ( 17.56713017795110332, -24.02660615158903923, 41.90057110130022977 ) ) ;
#4403=CARTESIAN_POINT ( 'NONE',  ( 14.68618260102867090, -26.77784494758310530, 1.962064221501000683 ) ) ;
#4407=CARTESIAN_POINT ( 'NONE',  ( 4.939584056586554084, 5.961151497827415824, 29.51773124056278164 ) ) ;
#4417=FACE_OUTER_BOUND ( 'NONE', #2511, .T. ) ;
#4420=DIRECTION ( 'NONE',  ( 0.000000000000000000, 0.000000000000000000, 1.000000000000000000 ) ) ;
#4430=DIRECTION ( 'NONE',  ( 0.000000000000000000, 1.000000000000000000, 1.224646799147350002E-16 ) ) ;
#4434=FACE_OUTER_BOUND ( 'NONE', #838, .T. ) ;
#4438=CARTESIAN_POINT ( 'NONE',  ( -5.500669204425239656, -13.50739036851649466, 60.35526053768147392 ) ) ;
#4441=CARTESIAN_POINT ( 'NONE',  ( 0.8003001391889992266, 3.992621007561997892, 24.16206422150099442 ) ) ;
#4444=CARTESIAN_POINT ( 'NONE',  ( 15.96229431146955058, -29.94371705786681304, 44.61892371905074128 ) ) ;
#4449=ORIENTED_EDGE ( 'NONE', *, *, #4988, .F. ) ;
#4450=AXIS2_PLACEMENT_3D ( 'NONE', #12282, #14722, #13356 ) ;
#4456=CARTESIAN_POINT ( 'NONE',  ( -35.49969986081099904, -19.50737899243800300, 55.93350807262480373 ) ) ;
#4458=CIRCLE ( 'NONE', #1046, 2.500000000000002220 ) ;
#4462=DIRECTION ( 'NONE',  ( -3.202566417187950042E-16, 0.000000000000000000, 1.000000000000000000 ) ) ;
#4464=CARTESIAN_POINT ( 'NONE',  ( 18.53245405280428315, -26.77692695969465220, 39.96206422150100224 ) ) ;
#4479=DIRECTION ( 'NONE',  ( 0.000000000000000000, 1.000000000000000000, 1.224646799147350002E-16 ) ) ;
#4482=DIRECTION ( 'NONE',  ( 0.000000000000000000, 2.168404344971008868E-16, -1.000000000000000000 ) ) ;
#4484=DIRECTION ( 'NONE',  ( 0.000000000000000000, -1.000000000000000000, -1.224646799147350002E-16 ) ) ;
#4494=ADVANCED_FACE ( 'NONE', ( #3074 ), #5357, .T. ) ;
#4501=CYLINDRICAL_SURFACE ( 'NONE', #13623, 2.500000000000000444 ) ;
#4502=CARTESIAN_POINT ( 'NONE',  ( -35.48358900502676505, 6.179576214079514962, 29.75589804712084074 ) ) ;
#4505=CARTESIAN_POINT ( 'NONE',  ( -15.49969986081099904, -32.00737899243800655, 61.71206422150100224 ) ) ;
#4506=ORIENTED_EDGE ( 'NONE', *, *, #12044, .F. ) ;
#4520=CARTESIAN_POINT ( 'NONE',  ( -28.78282149594069850, -32.00737899243799944, -10.85656391856669778 ) ) ;
#4527=CARTESIAN_POINT ( 'NONE',  ( 13.85920135429429934, -23.75737899243800300, 24.21206422150099868 ) ) ;
#4533=CIRCLE ( 'NONE', #8665, 19.00000000000000000 ) ;
#4538=ORIENTED_EDGE ( 'NONE', *, *, #334, .F. ) ;
#4539=CARTESIAN_POINT ( 'NONE',  ( 16.32012704356523614, -23.84468502132440904, 44.06002385016308409 ) ) ;
#4541=VECTOR ( 'NONE', #5118, 1000.000000000000000 ) ;
#4545=CYLINDRICAL_SURFACE ( 'NONE', #13253, 37.50000000000000000 ) ;
#4551=EDGE_CURVE ( 'NONE', #1400, #6240, #9033, .T. ) ;
#4555=CYLINDRICAL_SURFACE ( 'NONE', #201, 19.00000000000000000 ) ;
#4560=EDGE_CURVE ( 'NONE', #5342, #6219, #10262, .T. ) ;
#4571=EDGE_CURVE ( 'NONE', #11290, #2975, #8037, .T. ) ;
#4575=EDGE_CURVE ( 'NONE', #1508, #6681, #12700, .T. ) ;
#4582=ORIENTED_EDGE ( 'NONE', *, *, #5868, .T. ) ;
#4586=EDGE_CURVE ( 'NONE', #1150, #12465, #14929, .T. ) ;
#4588=FACE_OUTER_BOUND ( 'NONE', #9985, .T. ) ;
#4589=CARTESIAN_POINT ( 'NONE',  ( 9.000300139189000959, -27.00737899243800300, 5.212064221501000461 ) ) ;
#4596=CARTESIAN_POINT ( 'NONE',  ( -33.37651573321840459, -23.18484177525213497, 57.27215087687875439 ) ) ;
#4601=ORIENTED_EDGE ( 'NONE', *, *, #740, .F. ) ;
#4602=CARTESIAN_POINT ( 'NONE',  ( -25.33132850951382053, -11.70608228131975892, 60.40032490398561293 ) ) ;
#4605=CARTESIAN_POINT ( 'NONE',  ( -15.49969986081099904, 22.99262100756200056, 24.21206422150100224 ) ) ;
#4606=VERTEX_POINT ( 'NONE', #11712 ) ;
#4611=SHAPE_REPRESENTATION_RELATIONSHIP ( 'NONE' , 'NONE' ,  #6151, #4622 ) ;
#4612=DIRECTION ( 'NONE',  ( -1.000000000000000000, 3.922012711866029438E-32, -3.202566417187950042E-16 ) ) ;
#4618=VERTEX_POINT ( 'NONE', #14169 ) ;
#4619=CARTESIAN_POINT ( 'NONE',  ( -15.49969986081100082, 10.73810275766729561, 24.21206422150099868 ) ) ;
#4622=ADVANCED_BREP_SHAPE_REPRESENTATION ( '', ( #2515, #6789 ), #8750 ) ;
#4628=CARTESIAN_POINT ( 'NONE',  ( -15.49969986081099904, 0.9926210075619958939, 47.21206422150099513 ) ) ;
#4631=CARTESIAN_POINT ( 'NONE',  ( -15.49969986081099904, -13.50737899243800122, 61.71206422150099513 ) ) ;
#4636=CARTESIAN_POINT ( 'NONE',  ( -19.07799122369186762, -16.25188662377412641, -13.11718427892139438 ) ) ;
#4646=DIRECTION ( 'NONE',  ( -1.000000000000000000, 0.000000000000000000, 0.000000000000000000 ) ) ;
#4649=DIRECTION ( 'NONE',  ( 1.000000000000000000, -1.499759782661860071E-32, 1.224646799147350002E-16 ) ) ;
#4652=ORIENTED_EDGE ( 'NONE', *, *, #14304, .F. ) ;
#4664=CARTESIAN_POINT ( 'NONE',  ( -15.49969986081099904, 22.99262100756199700, 40.08706422150100224 ) ) ;
#4671=ORIENTED_EDGE ( 'NONE', *, *, #740, .T. ) ;
#4683=EDGE_CURVE ( 'NONE', #4771, #7197, #9417, .T. ) ;
#4702=EDGE_CURVE ( 'NONE', #4749, #12994, #3762, .T. ) ;
#4734=ORIENTED_EDGE ( 'NONE', *, *, #12370, .T. ) ;
#4742=CARTESIAN_POINT ( 'NONE',  ( -5.840324169876037530, -16.14984675272692627, 60.44710126137897532 ) ) ;
#4749=VERTEX_POINT ( 'NONE', #11959 ) ;
#4750=CARTESIAN_POINT ( 'NONE',  ( 7.200737182676100190, 4.873818854045000037, 20.51204286552489009 ) ) ;
#4757=ORIENTED_EDGE ( 'NONE', *, *, #198, .F. ) ;
#4762=CARTESIAN_POINT ( 'NONE',  ( -15.49969986081099904, 71.39262100756199914, 24.21206422150100579 ) ) ;
#4764=CARTESIAN_POINT ( 'NONE',  ( -17.75327345881522234, -9.601260756853328360, -13.22096152104317568 ) ) ;
#4771=VERTEX_POINT ( 'NONE', #13410 ) ;
#4790=DIRECTION ( 'NONE',  ( 0.000000000000000000, 2.168404344971008868E-16, -1.000000000000000000 ) ) ;
#4793=CARTESIAN_POINT ( 'NONE',  ( 22.00031467284088293, -30.25754668847291384, 24.42409879051542632 ) ) ;
#4800=EDGE_CURVE ( 'NONE', #12659, #15056, #12685, .T. ) ;
#4803=VERTEX_POINT ( 'NONE', #5000 ) ;
#4808=ORIENTED_EDGE ( 'NONE', *, *, #8077, .T. ) ;
#4815=CARTESIAN_POINT ( 'NONE',  ( -36.42585024326830734, 12.65779542994540208, 16.16206422150100153 ) ) ;
#4818=ADVANCED_FACE ( 'NONE', ( #14330 ), #7301, .F. ) ;
#4821=VECTOR ( 'NONE', #5307, 1000.000000000000000 ) ;
#4825=AXIS2_PLACEMENT_3D ( 'NONE', #293, #13304, #444 ) ;
#4826=CARTESIAN_POINT ( 'NONE',  ( -28.78282149594069850, -31.14135358865360104, 59.28069236156870403 ) ) ;
#4832=CIRCLE ( 'NONE', #5080, 37.50000000000000000 ) ;
#4834=ORIENTED_EDGE ( 'NONE', *, *, #11580, .F. ) ;
#4842=CARTESIAN_POINT ( 'NONE',  ( 18.30052381647702830, -25.27299409199407521, 7.969642897117474867 ) ) ;
#4851=DIRECTION ( 'NONE',  ( 1.000000000000000000, 0.000000000000000000, 0.000000000000000000 ) ) ;
#4889=CARTESIAN_POINT ( 'NONE',  ( 9.641860956753800949, -19.50737899243800300, 24.21206422150099868 ) ) ;
#4892=LINE ( 'NONE', #14216, #9377 ) ;
#4898=EDGE_CURVE ( 'NONE', #6978, #6240, #1199, .T. ) ;
#4900=CARTESIAN_POINT ( 'NONE',  ( -5.712217893050156370, -15.62993725438619208, 60.41238135938705511 ) ) ;
#4902=CARTESIAN_POINT ( 'NONE',  ( 17.66674905504159199, -29.89865791779061865, 6.711258755170492307 ) ) ;
#4915=ORIENTED_EDGE ( 'NONE', *, *, #14304, .T. ) ;
#4916=CARTESIAN_POINT ( 'NONE',  ( -32.76014075162859740, 10.68321993080349763, 16.26994987741149856 ) ) ;
#4917=CARTESIAN_POINT ( 'NONE',  ( -15.49969986081099904, 64.39262100756199914, 30.46206422150100934 ) ) ;
#4919=CARTESIAN_POINT ( 'NONE',  ( -19.76762875079388948, -12.05116796486094977, -13.04444617939184248 ) ) ;
#4924=EDGE_LOOP ( 'NONE', ( #4314, #13950, #14402, #6036 ) ) ;
#4939=CYLINDRICAL_SURFACE ( 'NONE', #5209, 5.250000000000000888 ) ;
#4942=CARTESIAN_POINT ( 'NONE',  ( 21.86105357425719475, -27.43463325034647937, 27.44097769609280846 ) ) ;
#4943=EDGE_CURVE ( 'NONE', #6725, #11422, #10486, .T. ) ;
#4951=CIRCLE ( 'NONE', #14952, 2.500000000000002220 ) ;
#4954=DIRECTION ( 'NONE',  ( 0.000000000000000000, 1.369518533665900312E-16, -1.000000000000000000 ) ) ;
#4955=CARTESIAN_POINT ( 'NONE',  ( 6.045543233663400073, 20.99262100756200056, 16.16206422150100153 ) ) ;
#4956=ORIENTED_EDGE ( 'NONE', *, *, #8205, .T. ) ;
#4959=VERTEX_POINT ( 'NONE', #10467 ) ;
#4973=DIRECTION ( 'NONE',  ( 0.000000000000000000, -1.000000000000000000, -1.224646799147350002E-16 ) ) ;
#4974=CARTESIAN_POINT ( 'NONE',  ( -15.49969986081099727, 20.99262100756199700, 39.83706422150100224 ) ) ;
#4982=EDGE_CURVE ( 'NONE', #11942, #12659, #14980, .T. ) ;
#4986=ORIENTED_EDGE ( 'NONE', *, *, #12189, .F. ) ;
#4988=EDGE_CURVE ( 'NONE', #5736, #700, #8004, .T. ) ;
#4990=EDGE_LOOP ( 'NONE', ( #10966, #5441 ) ) ;
#4994=CARTESIAN_POINT ( 'NONE',  ( -18.47333776534164684, -10.11719227462029735, -13.17042849143727778 ) ) ;
#4997=FACE_OUTER_BOUND ( 'NONE', #7873, .T. ) ;
#5000=CARTESIAN_POINT ( 'NONE',  ( -15.49969986081099904, 71.39262100756199914, 17.38382956928560219 ) ) ;
#5003=ORIENTED_EDGE ( 'NONE', *, *, #9701, .F. ) ;
#5005=ORIENTED_EDGE ( 'NONE', *, *, #2055, .F. ) ;
#5011=FACE_OUTER_BOUND ( 'NONE', #4990, .T. ) ;
#5019=DIRECTION ( 'NONE',  ( 0.000000000000000000, 1.000000000000000000, 1.224646799147350002E-16 ) ) ;
#5024=CARTESIAN_POINT ( 'NONE',  ( -15.49969986081099904, -13.50737899243800122, 6.712064221500998684 ) ) ;
#5038=AXIS2_PLACEMENT_3D ( 'NONE', #9765, #12069, #2580 ) ;
#5042=DIRECTION ( 'NONE',  ( 0.000000000000000000, 0.000000000000000000, 1.000000000000000000 ) ) ;
#5043=ADVANCED_FACE ( 'NONE', ( #3734, #9394 ), #8389, .T. ) ;
#5046=CIRCLE ( 'NONE', #13598, 3.250000000000002665 ) ;
#5047=CARTESIAN_POINT ( 'NONE',  ( 17.56619466861842227, -29.98873796865039765, 6.521841211496442803 ) ) ;
#5052=ORIENTED_EDGE ( 'NONE', *, *, #7570, .T. ) ;
#5054=VERTEX_POINT ( 'NONE', #8311 ) ;
#5057=EDGE_CURVE ( 'NONE', #14532, #11915, #4382, .T. ) ;
#5058=ORIENTED_EDGE ( 'NONE', *, *, #12976, .F. ) ;
#5062=CARTESIAN_POINT ( 'NONE',  ( -33.05408098453766996, 8.544173770627832454, 16.94260638916070150 ) ) ;
#5063=VECTOR ( 'NONE', #3543, 1000.000000000000000 ) ;
#5065=CARTESIAN_POINT ( 'NONE',  ( -12.90403152030055800, -3.849063734251706670, 61.62346604207912293 ) ) ;
#5067=EDGE_CURVE ( 'NONE', #1266, #12240, #8281, .T. ) ;
#5069=DIRECTION ( 'NONE',  ( 0.000000000000000000, -1.000000000000000000, -1.224646799147350002E-16 ) ) ;
#5080=AXIS2_PLACEMENT_3D ( 'NONE', #13388, #2896, #14677 ) ;
#5081=DIRECTION ( 'NONE',  ( 1.000000000000000000, 0.000000000000000000, 1.224646799147350002E-16 ) ) ;
#5087=CARTESIAN_POINT ( 'NONE',  ( -15.49969986081099904, 22.99262100756200411, 8.587064221501004013 ) ) ;
#5090=ORIENTED_EDGE ( 'NONE', *, *, #1430, .F. ) ;
#5092=DIRECTION ( 'NONE',  ( -1.000000000000000000, 1.499759782661860071E-32, -1.224646799147350002E-16 ) ) ;
#5095=CIRCLE ( 'NONE', #6530, 6.250000000000001776 ) ;
#5097=DIRECTION ( 'NONE',  ( 0.000000000000000000, 1.224646799147350002E-16, -1.000000000000000000 ) ) ;
#5102=LINE ( 'NONE', #11061, #6769 ) ;
#5107=DIRECTION ( 'NONE',  ( 0.000000000000000000, -2.168404344971007882E-16, 1.000000000000000000 ) ) ;
#5108=ORIENTED_EDGE ( 'NONE', *, *, #11580, .T. ) ;
#5109=CARTESIAN_POINT ( 'NONE',  ( 21.99848766979616599, -23.77809160205145034, 24.63628493690049481 ) ) ;
#5118=DIRECTION ( 'NONE',  ( -1.000000000000000000, 0.000000000000000000, 0.000000000000000000 ) ) ;
#5119=CARTESIAN_POINT ( 'NONE',  ( 22.00030013918900096, -27.00737899243800300, 39.96206422150099513 ) ) ;
#5122=CARTESIAN_POINT ( 'NONE',  ( -2.216578225681298697, -31.14135358865360104, 59.28069236156870403 ) ) ;
#5127=ORIENTED_EDGE ( 'NONE', *, *, #650, .F. ) ;
#5129=VECTOR ( 'NONE', #8770, 1000.000000000000000 ) ;
#5130=ADVANCED_FACE ( 'NONE', ( #7314 ), #219, .T. ) ;
#5135=DIRECTION ( 'NONE',  ( 0.000000000000000000, 1.000000000000000000, 1.224646799147350002E-16 ) ) ;
#5138=DIRECTION ( 'NONE',  ( -1.000000000000000000, 0.000000000000000000, 0.000000000000000000 ) ) ;
#5147=CARTESIAN_POINT ( 'NONE',  ( -12.75555302399369850, -9.928823230469003391, -13.18819869426426727 ) ) ;
#5152=VERTEX_POINT ( 'NONE', #6235 ) ;
#5156=ORIENTED_EDGE ( 'NONE', *, *, #12189, .T. ) ;
#5164=CARTESIAN_POINT ( 'NONE',  ( 4.685129763540130554, 6.083222336766384686, 18.77103779417431895 ) ) ;
#5168=EDGE_CURVE ( 'NONE', #4749, #7809, #1307, .T. ) ;
#5170=CARTESIAN_POINT ( 'NONE',  ( -31.79969986081099975, 3.992621007561997892, 24.16206422150099797 ) ) ;
#5175=AXIS2_PLACEMENT_3D ( 'NONE', #1626, #11110, #559 ) ;
#5176=CARTESIAN_POINT ( 'NONE',  ( 21.91129973042178491, -25.02583635234388026, 26.79684541854832247 ) ) ;
#5183=LINE ( 'NONE', #8996, #12271 ) ;
#5187=AXIS2_PLACEMENT_3D ( 'NONE', #7471, #4040, #3810 ) ;
#5190=CARTESIAN_POINT ( 'NONE',  ( 15.85054478794847554, -29.85571724108492120, 3.634072666459030820 ) ) ;
#5191=CARTESIAN_POINT ( 'NONE',  ( 13.85920135429429934, -27.00737899243800300, 20.96206422150100224 ) ) ;
#5200=CARTESIAN_POINT ( 'NONE',  ( -23.49969986081099904, -19.50737899243800300, 6.712064221500998684 ) ) ;
#5205=CARTESIAN_POINT ( 'NONE',  ( -33.11203844197629564, 8.260196310773684658, 17.08384978814601141 ) ) ;
#5206=CARTESIAN_POINT ( 'NONE',  ( -15.49969986081099904, -13.50737899243800122, 6.712064221500998684 ) ) ;
#5209=AXIS2_PLACEMENT_3D ( 'NONE', #12055, #5019, #14347 ) ;
#5230=CIRCLE ( 'NONE', #12322, 23.00000000000000000 ) ;
#5231=CARTESIAN_POINT ( 'NONE',  ( 13.85920135429429934, -27.00737899243800300, 8.462064221501000461 ) ) ;
#5232=CARTESIAN_POINT ( 'NONE',  ( -35.96525066421718009, 5.948560758909089863, 18.92081361401057649 ) ) ;
#5236=ORIENTED_EDGE ( 'NONE', *, *, #9575, .T. ) ;
#5239=ORIENTED_EDGE ( 'NONE', *, *, #7736, .T. ) ;
#5242=ORIENTED_EDGE ( 'NONE', *, *, #10015, .T. ) ;
#5256=CARTESIAN_POINT ( 'NONE',  ( 21.88649023383436187, -25.56571653516489206, 27.13259355918092552 ) ) ;
#5258=ORIENTED_EDGE ( 'NONE', *, *, #1317, .T. ) ;
#5269=DIRECTION ( 'NONE',  ( 0.000000000000000000, -1.000000000000000000, -1.224646799147350002E-16 ) ) ;
#5273=DIRECTION ( 'NONE',  ( 1.000000000000000000, 0.000000000000000000, 0.000000000000000000 ) ) ;
#5280=CARTESIAN_POINT ( 'NONE',  ( -15.49969986081099904, 3.992621007561997892, 24.21206422150100224 ) ) ;
#5281=B_SPLINE_CURVE_WITH_KNOTS ( 'NONE', 3,
 ( #1724, #4028, #8534, #509 ),
 .UNSPECIFIED., .F., .F.,
 ( 4, 4 ),
 ( 0.000000000000000000, 1.000000000000000000 ),
 .UNSPECIFIED. ) ;
#5296=CARTESIAN_POINT ( 'NONE',  ( -13.24439404687306165, -9.602254296713979898, -13.22085716751162288 ) ) ;
#5298=CARTESIAN_POINT ( 'NONE',  ( -15.49969986081099904, -19.50737899243800300, 24.21206422150100224 ) ) ;
#5300=CIRCLE ( 'NONE', #14092, 4.499999999999999112 ) ;
#5303=CARTESIAN_POINT ( 'NONE',  ( -35.92016838155372938, 5.970170166553522506, 18.89611068059123866 ) ) ;
#5307=DIRECTION ( 'NONE',  ( 7.070501591499380254E-17, 1.224646799147350002E-16, -1.000000000000000000 ) ) ;
#5310=LINE ( 'NONE', #9902, #1030 ) ;
#5311=EDGE_LOOP ( 'NONE', ( #8782, #10943, #1642, #14348 ) ) ;
#5312=AXIS2_PLACEMENT_3D ( 'NONE', #2502, #8235, #3728 ) ;
#5328=ORIENTED_EDGE ( 'NONE', *, *, #10090, .F. ) ;
#5338=DIRECTION ( 'NONE',  ( 0.000000000000000000, 0.000000000000000000, -1.000000000000000000 ) ) ;
#5342=VERTEX_POINT ( 'NONE', #9680 ) ;
#5348=ORIENTED_EDGE ( 'NONE', *, *, #12702, .F. ) ;
#5350=DIRECTION ( 'NONE',  ( -1.000000000000000000, 0.000000000000000000, 0.000000000000000000 ) ) ;
#5354=DIRECTION ( 'NONE',  ( 0.000000000000000000, 1.000000000000000000, 1.224646799147350002E-16 ) ) ;
#5357=CONICAL_SURFACE ( 'NONE', #726, 8.314203600725839749, 0.8578293273552097808 ) ;
#5361=CARTESIAN_POINT ( 'NONE',  ( -15.49969986081099904, 20.99262100756200056, 24.21206422150099868 ) ) ;
#5363=CARTESIAN_POINT ( 'NONE',  ( 14.95717157845075818, -28.53344780807426773, 46.08993571701573444 ) ) ;
#5381=ORIENTED_EDGE ( 'NONE', *, *, #15020, .F. ) ;
#5382=VERTEX_POINT ( 'NONE', #11823 ) ;
#5383=PLANE ( 'NONE',  #14948 ) ;
#5386=CIRCLE ( 'NONE', #13223, 6.828234652215419587 ) ;
#5395=FACE_OUTER_BOUND ( 'NONE', #7602, .T. ) ;
#5406=CARTESIAN_POINT ( 'NONE',  ( 0.8003001391889992266, 11.99262100756199878, 32.26206422150099939 ) ) ;
#5407=CARTESIAN_POINT ( 'NONE',  ( 22.00030013918900096, -27.00737899243800300, 24.21206422150099868 ) ) ;
#5420=CARTESIAN_POINT ( 'NONE',  ( 9.000300139189000959, -27.00737899243800300, 43.21206422150100224 ) ) ;
#5429=CYLINDRICAL_SURFACE ( 'NONE', #895, 8.000000000000000000 ) ;
#5438=VECTOR ( 'NONE', #13186, 1000.000000000000000 ) ;
#5440=CYLINDRICAL_SURFACE ( 'NONE', #10607, 10.00000000000000000 ) ;
#5441=ORIENTED_EDGE ( 'NONE', *, *, #334, .T. ) ;
#5442=CARTESIAN_POINT ( 'NONE',  ( 9.000300139189000959, -19.50737899243800300, 24.21206422150099868 ) ) ;
#5452=DIRECTION ( 'NONE',  ( 0.000000000000000000, 0.000000000000000000, 1.000000000000000000 ) ) ;
#5457=DIRECTION ( 'NONE',  ( 0.000000000000000000, 1.224646799147350002E-16, -1.000000000000000000 ) ) ;
#5466=CARTESIAN_POINT ( 'NONE',  ( -15.49969986081099904, 70.81438635534659909, 17.96206422150100579 ) ) ;
#5470=CARTESIAN_POINT ( 'NONE',  ( 4.965850942597395346, 5.948560758908072010, 29.50331482898986835 ) ) ;
#5476=CARTESIAN_POINT ( 'NONE',  ( 1.760741030006599317, 10.68321993080349763, 32.15417856559049881 ) ) ;
#5485=LINE ( 'NONE', #4345, #5129 ) ;
#5486=CARTESIAN_POINT ( 'NONE',  ( 13.85920135429429934, -27.00737899243800300, 45.71206422150100224 ) ) ;
#5487=( BOUNDED_CURVE ( )  B_SPLINE_CURVE ( 3, ( #6458, #1657, #1813, #10990 ),
 .UNSPECIFIED., .F., .T. ) 
 B_SPLINE_CURVE_WITH_KNOTS ( ( 4, 4 ),
 ( 5.074465175390796112, 5.274925224928544765 ),
 .UNSPECIFIED. ) 
 CURVE ( )  GEOMETRIC_REPRESENTATION_ITEM ( )  RATIONAL_B_SPLINE_CURVE ( ( 1.000000000000000000, 0.9966541165307394312, 0.9966541165307394312, 1.000000000000000000 ) ) 
 REPRESENTATION_ITEM ( '' )  );
#5500=EDGE_CURVE ( 'NONE', #1107, #1827, #11279, .T. ) ;
#5503=EDGE_CURVE ( 'NONE', #8578, #12931, #2719, .T. ) ;
#5504=CARTESIAN_POINT ( 'NONE',  ( -5.502541905842194936, -13.18104144132555078, 60.35493120382419363 ) ) ;
#5507=EDGE_CURVE ( 'NONE', #11542, #364, #5310, .T. ) ;
#5509=CARTESIAN_POINT ( 'NONE',  ( 17.94012796689997558, -29.55659949177507073, 41.18440502598058828 ) ) ;
#5513=ORIENTED_EDGE ( 'NONE', *, *, #7452, .T. ) ;
#5518=ADVANCED_FACE ( 'NONE', ( #647, #9971 ), #5383, .F. ) ;
#5526=CARTESIAN_POINT ( 'NONE',  ( 15.30804704745935219, -24.78610190351696119, 45.59350641046059849 ) ) ;
#5528=LINE ( 'NONE', #9044, #3833 ) ;
#5529=EDGE_LOOP ( 'NONE', ( #11024, #13365, #10902, #10652 ) ) ;
#5534=CIRCLE ( 'NONE', #6745, 6.250000000000001776 ) ;
#5536=DIRECTION ( 'NONE',  ( 0.000000000000000000, -9.130123557772668334E-17, 1.000000000000000000 ) ) ;
#5539=LINE ( 'NONE', #13734, #2784 ) ;
#5554=CIRCLE ( 'NONE', #6767, 15.62500000000000000 ) ;
#5563=LINE ( 'NONE', #10236, #13064 ) ;
#5570=CYLINDRICAL_SURFACE ( 'NONE', #2013, 19.00000000000000000 ) ;
#5574=CARTESIAN_POINT ( 'NONE',  ( -7.977563667684565374, -6.908081013795536407, 60.95049943312243812 ) ) ;
#5580=ORIENTED_EDGE ( 'NONE', *, *, #12456, .F. ) ;
#5581=CARTESIAN_POINT ( 'NONE',  ( 18.10161036139083990, -29.26328343019616085, 40.86242124114806273 ) ) ;
#5589=LINE ( 'NONE', #859, #12166 ) ;
#5591=B_SPLINE_CURVE_WITH_KNOTS ( 'NONE', 3,
 ( #8219, #2569, #4942, #3715, #11740, #7298, #12907, #9525, #3563, #2419, #1346, #11897, #6143, #1423, #1262, #5920, #4793, #14350, #6070, #10599, #10754, #3864, #278, #14120, #3640, #9602, #3792, #8451, #1945, #14570, #9756, #14423, #12280, #11129 ),
 .UNSPECIFIED., .F., .F.,
 ( 4, 2, 2, 2, 2, 2, 2, 2, 2, 2, 2, 2, 2, 2, 2, 2, 4 ),
 ( 0.000000000000000000, 0.0006405057738602453962, 0.001281011547720490792, 0.001921517321580736189, 0.002562023095440981585, 0.003202528869301226981, 0.003843034643161472377, 0.004483540417021717774, 0.005124046190881963170, 0.005764551964742208566, 0.006405057738602453962, 0.007045563512462699358, 0.007686069286322944755, 0.008326575060183191018, 0.008967080834043435547, 0.009607586607903680076, 0.01024809238176392634 ),
 .UNSPECIFIED. ) ;
#5616=ORIENTED_EDGE ( 'NONE', *, *, #4898, .F. ) ;
#5619=ADVANCED_FACE ( 'NONE', ( #13875 ), #4545, .T. ) ;
#5621=VERTEX_POINT ( 'NONE', #13802 ) ;
#5627=DIRECTION ( 'NONE',  ( 1.000000000000000000, -1.499759782661860071E-32, 1.224646799147350002E-16 ) ) ;
#5634=DIRECTION ( 'NONE',  ( -1.000000000000000000, -3.632077277826439854E-16, 0.000000000000000000 ) ) ;
#5635=CARTESIAN_POINT ( 'NONE',  ( -35.18530787408519700, 11.99262100756819827, 32.26206422150099939 ) ) ;
#5638=CARTESIAN_POINT ( 'NONE',  ( -33.37394235882850069, 7.183219930803497633, 30.65500261342018007 ) ) ;
#5639=CARTESIAN_POINT ( 'NONE',  ( 22.00030013918900096, -27.00737899243800300, 8.462064221501000461 ) ) ;
#5642=CYLINDRICAL_SURFACE ( 'NONE', #4246, 2.499999999999998668 ) ;
#5650=DIRECTION ( 'NONE',  ( 0.000000000000000000, 0.000000000000000000, -1.000000000000000000 ) ) ;
#5653=CARTESIAN_POINT ( 'NONE',  ( -31.79969986081099975, 3.992621007561997892, 24.26206422150100650 ) ) ;
#5656=CARTESIAN_POINT ( 'NONE',  ( 16.55417383883170857, -30.23012602008740757, 43.67615232897840372 ) ) ;
#5658=CARTESIAN_POINT ( 'NONE',  ( -25.36033965610130991, -11.87119290823832252, 60.39242409889988750 ) ) ;
#5662=AXIS2_PLACEMENT_3D ( 'NONE', #8047, #8970, #3167 ) ;
#5673=EDGE_LOOP ( 'NONE', ( #110, #10532, #5381, #12847, #12734 ) ) ;
#5686=ADVANCED_FACE ( 'NONE', ( #11354 ), #10352, .T. ) ;
#5689=ADVANCED_FACE ( 'NONE', ( #11275 ), #2021, .T. ) ;
#5693=CARTESIAN_POINT ( 'NONE',  ( 2.374542637206501272, 7.183219930803497633, 30.65500261342018007 ) ) ;
#5694=ORIENTED_EDGE ( 'NONE', *, *, #5168, .T. ) ;
#5698=EDGE_CURVE ( 'NONE', #9250, #8623, #8435, .T. ) ;
#5704=CARTESIAN_POINT ( 'NONE',  ( -15.49969986081099904, -2.007378992438005216, 61.71206422150100934 ) ) ;
#5706=CARTESIAN_POINT ( 'NONE',  ( 7.500245791298697284, 3.992621007561997892, 24.16206422150099442 ) ) ;
#5723=CIRCLE ( 'NONE', #3760, 28.00000000000000000 ) ;
#5732=DIRECTION ( 'NONE',  ( 0.000000000000000000, 1.369518533665900312E-16, -1.000000000000000000 ) ) ;
#5736=VERTEX_POINT ( 'NONE', #4619 ) ;
#5738=CARTESIAN_POINT ( 'NONE',  ( -25.43050946283875646, -12.36304378589120745, 60.37322180574037134 ) ) ;
#5745=DIRECTION ( 'NONE',  ( 0.000000000000000000, 1.850371707708594316E-16, -1.000000000000000000 ) ) ;
#5764=DIRECTION ( 'NONE',  ( -1.000000000000000000, 0.000000000000000000, 0.000000000000000000 ) ) ;
#5791=EDGE_LOOP ( 'NONE', ( #8798, #11859, #340, #12751, #1656, #6339, #5328 ) ) ;
#5793=EDGE_LOOP ( 'NONE', ( #7386, #874, #1373, #6825, #3334 ) ) ;
#5801=CARTESIAN_POINT ( 'NONE',  ( -15.49969986081099904, 0.9926210075619958939, 47.21206422150099513 ) ) ;
#5809=LINE ( 'NONE', #6537, #301 ) ;
#5812=CARTESIAN_POINT ( 'NONE',  ( -17.77108926314113191, -3.766888484081842403, 61.64460505631792842 ) ) ;
#5820=CARTESIAN_POINT ( 'NONE',  ( 17.66455568904909512, -24.11403567254761171, 6.707112557092502314 ) ) ;
#5825=CARTESIAN_POINT ( 'NONE',  ( -14.04983158491594075, -17.77761107388303685, -13.26088994341721694 ) ) ;
#5829=ORIENTED_EDGE ( 'NONE', *, *, #10184, .F. ) ;
#5838=CARTESIAN_POINT ( 'NONE',  ( -38.49964551292070070, 3.992621007561997892, 24.26206422150100650 ) ) ;
#5841=DIRECTION ( 'NONE',  ( 0.000000000000000000, 1.000000000000000000, 1.224646799147350002E-16 ) ) ;
#5868=EDGE_CURVE ( 'NONE', #10153, #5342, #10548, .T. ) ;
#5878=CARTESIAN_POINT ( 'NONE',  ( 7.498862047384196927, 3.992621007561999669, 23.52554352489782730 ) ) ;
#5888=AXIS2_PLACEMENT_3D ( 'NONE', #8437, #13823, #13970 ) ;
#5891=EDGE_CURVE ( 'NONE', #10757, #2844, #2491, .T. ) ;
#5892=CARTESIAN_POINT ( 'NONE',  ( -18.24212484032476667, -9.927510438464585363, -13.18832502026138620 ) ) ;
#5899=VERTEX_POINT ( 'NONE', #3999 ) ;
#5904=DIRECTION ( 'NONE',  ( -1.000000000000000000, 0.000000000000000000, 0.000000000000000000 ) ) ;
#5909=CIRCLE ( 'NONE', #14712, 3.249999999999999556 ) ;
#5914=CARTESIAN_POINT ( 'NONE',  ( 13.85920135429429934, -27.00737899243800300, 43.21206422150100224 ) ) ;
#5918=ORIENTED_EDGE ( 'NONE', *, *, #7662, .F. ) ;
#5919=EDGE_LOOP ( 'NONE', ( #7562, #8899, #13932, #9486 ) ) ;
#5920=CARTESIAN_POINT ( 'NONE',  ( 21.99848181214818155, -30.23659088485334934, 24.63578152807335897 ) ) ;
#5923=CIRCLE ( 'NONE', #10573, 23.00000000000000000 ) ;
#5929=LINE ( 'NONE', #59, #8245 ) ;
#5931=PLANE ( 'NONE',  #8198 ) ;
#5932=CARTESIAN_POINT ( 'NONE',  ( -33.43612459426397265, 11.05255549920671321, 32.21545598376612674 ) ) ;
#5936=CIRCLE ( 'NONE', #1312, 23.00000000000000000 ) ;
#5942=EDGE_LOOP ( 'NONE', ( #4538, #4915, #13118, #13574 ) ) ;
#5944=PLANE ( 'NONE',  #12032 ) ;
#5948=FACE_BOUND ( 'NONE', #2484, .T. ) ;
#5950=FACE_OUTER_BOUND ( 'NONE', #14101, .T. ) ;
#5951=VECTOR ( 'NONE', #2206, 1000.000000000000000 ) ;
#5958=ORIENTED_EDGE ( 'NONE', *, *, #723, .F. ) ;
#5967=AXIS2_PLACEMENT_3D ( 'NONE', #2560, #7209, #11889 ) ;
#5971=VECTOR ( 'NONE', #3093, 1000.000000000000114 ) ;
#5977=CARTESIAN_POINT ( 'NONE',  ( 13.85920135429429934, -27.00737899243800300, 2.712064221501000461 ) ) ;
#5987=DIRECTION ( 'NONE',  ( -1.000000000000000000, 0.000000000000000000, 0.000000000000000000 ) ) ;
#5989=CARTESIAN_POINT ( 'NONE',  ( 9.000300139189000959, -27.00737899243800300, 5.212064221501000461 ) ) ;
#5993=DIRECTION ( 'NONE',  ( 3.632077277826439854E-16, -1.000000000000000000, 0.000000000000000000 ) ) ;
#5994=CARTESIAN_POINT ( 'NONE',  ( -24.59223421123983400, -17.67354377200967264, 60.59320803929022503 ) ) ;
#5998=EDGE_CURVE ( 'NONE', #8595, #13469, #5589, .T. ) ;
#5999=ORIENTED_EDGE ( 'NONE', *, *, #13101, .T. ) ;
#6008=CARTESIAN_POINT ( 'NONE',  ( -2.216578225681298697, -31.14135358865360104, 59.28069236156870403 ) ) ;
#6018=AXIS2_PLACEMENT_3D ( 'NONE', #1976, #9998, #13530 ) ;
#6019=CARTESIAN_POINT ( 'NONE',  ( -6.097673344397686712, -16.91980966733272140, 60.51440242979897022 ) ) ;
#6021=CARTESIAN_POINT ( 'NONE',  ( 22.00030013918900096, -27.00737899243800300, 45.71206422150100224 ) ) ;
#6025=LINE ( 'NONE', #14308, #821 ) ;
#6036=ORIENTED_EDGE ( 'NONE', *, *, #9823, .F. ) ;
#6042=CARTESIAN_POINT ( 'NONE',  ( -15.49969986081099371, -9.007378992438001220, -13.28793577849899599 ) ) ;
#6048=EDGE_LOOP ( 'NONE', ( #8393, #7180, #161, #8935 ) ) ;
#6050=ORIENTED_EDGE ( 'NONE', *, *, #7206, .T. ) ;
#6053=VECTOR ( 'NONE', #925, 1000.000000000000000 ) ;
#6070=CARTESIAN_POINT ( 'NONE',  ( 21.99843046478421371, -30.23599839927906530, 23.78383503728017345 ) ) ;
#6072=ORIENTED_EDGE ( 'NONE', *, *, #14196, .T. ) ;
#6077=CARTESIAN_POINT ( 'NONE',  ( 22.00030013918900096, -27.00737899243800300, 43.21206422150100224 ) ) ;
#6087=CARTESIAN_POINT ( 'NONE',  ( -15.49969986081099904, 71.39262100756199914, 24.21206422150100579 ) ) ;
#6093=EDGE_CURVE ( 'NONE', #14313, #5899, #7748, .T. ) ;
#6094=CARTESIAN_POINT ( 'NONE',  ( -35.18530787408279537, 11.99262100756689620, 16.16206422150100153 ) ) ;
#6112=ADVANCED_FACE ( 'NONE', ( #7104 ), #3450, .T. ) ;
#6118=CARTESIAN_POINT ( 'NONE',  ( -11.02913861065588641, -14.09954045717994653, -13.02054842795066314 ) ) ;
#6121=FILL_AREA_STYLE_COLOUR ( '', #9451 ) ;
#6122=ORIENTED_EDGE ( 'NONE', *, *, #10829, .F. ) ;
#6124=CARTESIAN_POINT ( 'NONE',  ( -15.49969986081099904, 9.919219809770901009, 5.212064221501000461 ) ) ;
#6129=ADVANCED_FACE ( 'NONE', ( #10491 ), #19, .T. ) ;
#6135=FACE_OUTER_BOUND ( 'NONE', #8462, .T. ) ;
#6141=ORIENTED_EDGE ( 'NONE', *, *, #14356, .T. ) ;
#6143=CARTESIAN_POINT ( 'NONE',  ( 21.97318612132534099, -29.92907000624635927, 25.65138358613589276 ) ) ;
#6145=ORIENTED_EDGE ( 'NONE', *, *, #10015, .F. ) ;
#6151=SHAPE_REPRESENTATION ( 'Tapered Toolholder Shank', ( #6789 ), #8750 ) ;
#6152=VECTOR ( 'NONE', #4851, 1000.000000000000000 ) ;
#6155=CARTESIAN_POINT ( 'NONE',  ( 7.444842330671914254, 4.142642748846463441, 25.83772173559120944 ) ) ;
#6170=ORIENTED_EDGE ( 'NONE', *, *, #2073, .F. ) ;
#6173=ADVANCED_FACE ( 'NONE', ( #8416 ), #11864, .T. ) ;
#6175=CARTESIAN_POINT ( 'NONE',  ( 13.85920135429429934, -27.00737899243800300, 43.21206422150100224 ) ) ;
#6177=CARTESIAN_POINT ( 'NONE',  ( 13.85920135429429934, -27.00737899243800300, 24.21206422150099868 ) ) ;
#6179=CARTESIAN_POINT ( 'NONE',  ( 18.53245405280430802, -27.24065255069785252, 8.462064221501002237 ) ) ;
#6180=ORIENTED_EDGE ( 'NONE', *, *, #8823, .F. ) ;
#6184=CARTESIAN_POINT ( 'NONE',  ( 2.013526631810669265, 8.758714366253697037, 31.58011097299207037 ) ) ;
#6201=LINE ( 'NONE', #484, #8826 ) ;
#6208=ORIENTED_EDGE ( 'NONE', *, *, #12370, .F. ) ;
#6209=ORIENTED_EDGE ( 'NONE', *, *, #2972, .F. ) ;
#6212=CARTESIAN_POINT ( 'NONE',  ( -15.49969986081099904, 70.81438635534659909, 24.21206422150100579 ) ) ;
#6213=DIRECTION ( 'NONE',  ( 0.000000000000000000, 1.131341397376178572E-16, -1.000000000000000000 ) ) ;
#6218=CARTESIAN_POINT ( 'NONE',  ( -37.58940743239428173, 5.168430268690432428, 19.97516569973667089 ) ) ;
#6219=VERTEX_POINT ( 'NONE', #10562 ) ;
#6226=DIRECTION ( 'NONE',  ( 0.000000000000000000, -1.000000000000000000, -1.224646799147350002E-16 ) ) ;
#6230=LINE ( 'NONE', #10684, #2041 ) ;
#6235=CARTESIAN_POINT ( 'NONE',  ( 2.374542637206501272, 7.183219930803497633, 17.76912582958182085 ) ) ;
#6237=ORIENTED_EDGE ( 'NONE', *, *, #6247, .F. ) ;
#6238=AXIS2_PLACEMENT_3D ( 'NONE', #981, #3572, #11606 ) ;
#6240=VERTEX_POINT ( 'NONE', #3493 ) ;
#6241=CARTESIAN_POINT ( 'NONE',  ( 13.85920135429429934, -27.00737899243800300, 1.962064221501000683 ) ) ;
#6246=LINE ( 'NONE', #6021, #4541 ) ;
#6247=EDGE_CURVE ( 'NONE', #13484, #1625, #5929, .T. ) ;
#6264=ORIENTED_EDGE ( 'NONE', *, *, #3004, .F. ) ;
#6270=CIRCLE ( 'NONE', #12647, 2.499999999999998668 ) ;
#6271=CARTESIAN_POINT ( 'NONE',  ( -15.49969986081099371, -32.00737899243799234, -13.28793577849899599 ) ) ;
#6293=CARTESIAN_POINT ( 'NONE',  ( -34.10648070438527668, 6.836425395143246320, 18.03001900748674657 ) ) ;
#6313=CARTESIAN_POINT ( 'NONE',  ( 22.00029349158540626, -23.75745569556128345, 24.42532365904204283 ) ) ;
#6323=VECTOR ( 'NONE', #9384, 1000.000000000000000 ) ;
#6325=DIRECTION ( 'NONE',  ( 0.000000000000000000, 0.000000000000000000, 1.000000000000000000 ) ) ;
#6326=CARTESIAN_POINT ( 'NONE',  ( 16.20074900174340726, -30.09470171131693661, 4.177619646552957811 ) ) ;
#6329=CARTESIAN_POINT ( 'NONE',  ( -32.97257072231203523, 8.982922429331180680, 31.67529590550448404 ) ) ;
#6339=ORIENTED_EDGE ( 'NONE', *, *, #13296, .F. ) ;
#6342=CARTESIAN_POINT ( 'NONE',  ( -33.30392703919734743, 7.441414002149839391, 17.57488669123580749 ) ) ;
#6353=VERTEX_POINT ( 'NONE', #11906 ) ;
#6355=ORIENTED_EDGE ( 'NONE', *, *, #12044, .T. ) ;
#6359=DIRECTION ( 'NONE',  ( 0.000000000000000000, -2.168404344971008868E-16, 1.000000000000000000 ) ) ;
#6362=ORIENTED_EDGE ( 'NONE', *, *, #14575, .F. ) ;
#6366=ORIENTED_EDGE ( 'NONE', *, *, #5057, .T. ) ;
#6368=EDGE_CURVE ( 'NONE', #1908, #1644, #5102, .T. ) ;
#6372=CARTESIAN_POINT ( 'NONE',  ( 9.000300139189000959, -27.00737899243800300, 40.71206422150099513 ) ) ;
#6373=FACE_OUTER_BOUND ( 'NONE', #9379, .T. ) ;
#6377=DIRECTION ( 'NONE',  ( 0.000000000000000000, 1.000000000000000000, 0.000000000000000000 ) ) ;
#6382=EDGE_CURVE ( 'NONE', #3863, #4618, #5281, .T. ) ;
#6387=DIRECTION ( 'NONE',  ( 0.000000000000000000, 1.131341397376178572E-16, -1.000000000000000000 ) ) ;
#6394=DIRECTION ( 'NONE',  ( 0.000000000000000000, -2.185478394931410082E-16, 1.000000000000000000 ) ) ;
#6404=EDGE_CURVE ( 'NONE', #3050, #8123, #3117, .T. ) ;
#6406=ORIENTED_EDGE ( 'NONE', *, *, #3749, .F. ) ;
#6411=LINE ( 'NONE', #11092, #1176 ) ;
#6413=B_SPLINE_CURVE_WITH_KNOTS ( 'NONE', 3,
 ( #6094, #3741, #4815, #1592 ),
 .UNSPECIFIED., .F., .F.,
 ( 4, 4 ),
 ( 0.01169941957287599921, 0.01381006638855979997 ),
 .UNSPECIFIED. ) ;
#6419=AXIS2_PLACEMENT_3D ( 'NONE', #10390, #9009, #3354 ) ;
#6421=ADVANCED_FACE ( 'NONE', ( #8378 ), #13068, .F. ) ;
#6433=CARTESIAN_POINT ( 'NONE',  ( -12.10927446591014700, -10.53397642412856072, -13.13493504121917432 ) ) ;
#6434=EDGE_CURVE ( 'NONE', #8805, #10153, #7256, .T. ) ;
#6437=CARTESIAN_POINT ( 'NONE',  ( -15.49969986081099904, 4.873818854045000037, 24.21206422150099868 ) ) ;
#6451=CARTESIAN_POINT ( 'NONE',  ( 4.484189283470824350, 6.179576214047821203, 18.66823039591405120 ) ) ;
#6453=AXIS2_PLACEMENT_3D ( 'NONE', #3742, #651, #13294 ) ;
#6456=PLANE ( 'NONE',  #7403 ) ;
#6458=CARTESIAN_POINT ( 'NONE',  ( -28.78282149594069850, -31.14135358865360104, -10.85656391856669778 ) ) ;
#6462=CARTESIAN_POINT ( 'NONE',  ( 21.88645104390297647, -25.56672272642999033, 21.29103469435690954 ) ) ;
#6473=CARTESIAN_POINT ( 'NONE',  ( -32.76014075162859740, 10.68321993080349763, 32.15417856559049881 ) ) ;
#6484=VECTOR ( 'NONE', #14992, 1000.000000000000000 ) ;
#6490=CARTESIAN_POINT ( 'NONE',  ( 13.85920135429429934, -27.00737899243800300, 26.71206422150099868 ) ) ;
#6493=AXIS2_PLACEMENT_3D ( 'NONE', #81, #11850, #3670 ) ;
#6500=CARTESIAN_POINT ( 'NONE',  ( 1.785016747259931202, 10.36523356804368845, 16.32270781623988753 ) ) ;
#6502=AXIS2_PLACEMENT_3D ( 'NONE', #7118, #13192, #3695 ) ;
#6503=CARTESIAN_POINT ( 'NONE',  ( -15.49969986081099371, -9.007378992438001220, -13.28793577849899599 ) ) ;
#6504=EDGE_CURVE ( 'NONE', #12569, #4606, #1881, .T. ) ;
#6507=AXIS2_PLACEMENT_3D ( 'NONE', #750, #5338, #901 ) ;
#6508=ADVANCED_FACE ( 'NONE', ( #7902 ), #12508, .F. ) ;
#6513=LINE ( 'NONE', #12197, #10454 ) ;
#6521=EDGE_CURVE ( 'NONE', #10220, #8595, #14954, .T. ) ;
#6528=DIRECTION ( 'NONE',  ( 1.000000000000000000, -1.499759782661860071E-32, 1.224646799147350002E-16 ) ) ;
#6530=AXIS2_PLACEMENT_3D ( 'NONE', #2032, #11364, #6905 ) ;
#6531=AXIS2_PLACEMENT_3D ( 'NONE', #7423, #8570, #405 ) ;
#6534=DIRECTION ( 'NONE',  ( 0.000000000000000000, 0.000000000000000000, 1.000000000000000000 ) ) ;
#6537=CARTESIAN_POINT ( 'NONE',  ( -31.79969986081099975, 11.99262100756199878, 32.26206422150099939 ) ) ;
#6538=CARTESIAN_POINT ( 'NONE',  ( 21.98614235536664197, -23.92397303140615605, 25.26083157490126752 ) ) ;
#6543=CYLINDRICAL_SURFACE ( 'NONE', #13918, 3.250000000000002665 ) ;
#6545=EDGE_CURVE ( 'NONE', #3162, #4803, #14880, .T. ) ;
#6547=FACE_OUTER_BOUND ( 'NONE', #9414, .T. ) ;
#6551=VERTEX_POINT ( 'NONE', #10125 ) ;
#6552=CARTESIAN_POINT ( 'NONE',  ( -32.78441646887873873, 10.36523356808538665, 32.10142062676905539 ) ) ;
#6553=CARTESIAN_POINT ( 'NONE',  ( -31.79969986081099975, 20.99262100756200056, 32.26206422150099939 ) ) ;
#6556=ORIENTED_EDGE ( 'NONE', *, *, #9969, .F. ) ;
#6561=AXIS2_PLACEMENT_3D ( 'NONE', #3842, #8726, #8505 ) ;
#6571=EDGE_LOOP ( 'NONE', ( #11707, #12033, #9712, #6362 ) ) ;
#6574=EDGE_CURVE ( 'NONE', #2938, #13270, #2554, .T. ) ;
#6585=DIRECTION ( 'NONE',  ( 0.000000000000000000, 1.000000000000000000, 1.224646799147350002E-16 ) ) ;
#6593=AXIS2_PLACEMENT_3D ( 'NONE', #5206, #12249, #11172 ) ;
#6594=CARTESIAN_POINT ( 'NONE',  ( 3.105701218396447860, 6.837078596092822202, 18.02952760507402985 ) ) ;
#6595=CARTESIAN_POINT ( 'NONE',  ( 0.8918609567539013128, -25.75737899243799944, -123.9247733198440073 ) ) ;
#6597=UNCERTAINTY_MEASURE_WITH_UNIT (LENGTH_MEASURE( 1.000000000000000082E-05 ), #9580, 'distance_accuracy_value', 'NONE');
#6603=DIRECTION ( 'NONE',  ( 0.000000000000000000, -9.130123557772668334E-17, 1.000000000000000000 ) ) ;
#6607=EDGE_CURVE ( 'NONE', #1579, #12952, #12226, .T. ) ;
#6610=CARTESIAN_POINT ( 'NONE',  ( 9.000300139189000959, -27.00737899243800300, 24.21206422150099868 ) ) ;
#6615=DIRECTION ( 'NONE',  ( 0.000000000000000000, -1.000000000000000000, -1.224646799147350002E-16 ) ) ;
#6619=CARTESIAN_POINT ( 'NONE',  ( -15.49969986081099904, 70.81438635534659909, 17.96206422150100579 ) ) ;
#6629=CARTESIAN_POINT ( 'NONE',  ( 22.00030013918900096, -27.00737899243800300, 24.21206422150099868 ) ) ;
#6632=CARTESIAN_POINT ( 'NONE',  ( 13.85920135429429934, -27.00737899243800300, 24.21206422150099868 ) ) ;
#6633=DIRECTION ( 'NONE',  ( 0.000000000000000000, -1.000000000000000000, -1.224646799147350002E-16 ) ) ;
#6637=AXIS2_PLACEMENT_3D ( 'NONE', #4020, #8394, #4244 ) ;
#6642=LINE ( 'NONE', #11397, #6053 ) ;
#6649=CARTESIAN_POINT ( 'NONE',  ( -18.09470815789902076, -3.848709554607572692, 61.62351371178731796 ) ) ;
#6651=ORIENTED_EDGE ( 'NONE', *, *, #8676, .T. ) ;
#6655=DIRECTION ( 'NONE',  ( 3.202566417187950042E-16, 1.224646799147350002E-16, -1.000000000000000000 ) ) ;
#6660=AXIS2_PLACEMENT_3D ( 'NONE', #14162, #2456, #9644 ) ;
#6665=CARTESIAN_POINT ( 'NONE',  ( 15.96494998288805789, -24.06893396188195311, 44.61485892283481292 ) ) ;
#6676=CARTESIAN_POINT ( 'NONE',  ( 14.82649946315277312, -25.88651038688090367, 2.153413930940738297 ) ) ;
#6680=CARTESIAN_POINT ( 'NONE',  ( 6.920290371738591517, 5.009117329185531986, 28.17596432838387699 ) ) ;
#6681=VERTEX_POINT ( 'NONE', #8720 ) ;
#6684=ORIENTED_EDGE ( 'NONE', *, *, #14200, .F. ) ;
#6685=EDGE_LOOP ( 'NONE', ( #6264, #630 ) ) ;
#6696=EDGE_CURVE ( 'NONE', #14421, #11355, #3867, .T. ) ;
#6700=EDGE_CURVE ( 'NONE', #13514, #1579, #9941, .T. ) ;
#6705=DIRECTION ( 'NONE',  ( -1.000000000000000000, 0.000000000000000000, 0.000000000000000000 ) ) ;
#6714=DIRECTION ( 'NONE',  ( -1.000000000000000000, 0.000000000000000000, 0.000000000000000000 ) ) ;
#6725=VERTEX_POINT ( 'NONE', #14465 ) ;
#6726=AXIS2_PLACEMENT_3D ( 'NONE', #5407, #1977, #9924 ) ;
#6734=FACE_OUTER_BOUND ( 'NONE', #9467, .T. ) ;
#6737=EDGE_LOOP ( 'NONE', ( #6556, #13077 ) ) ;
#6739=EDGE_LOOP ( 'NONE', ( #12318, #6180, #45, #7724, #9946, #10461, #10671, #14847, #8656, #6355, #7832, #9750, #12059, #14895, #13579 ) ) ;
#6740=ORIENTED_EDGE ( 'NONE', *, *, #7653, .F. ) ;
#6742=ORIENTED_EDGE ( 'NONE', *, *, #7381, .F. ) ;
#6744=EDGE_CURVE ( 'NONE', #14381, #13214, #9877, .T. ) ;
#6745=AXIS2_PLACEMENT_3D ( 'NONE', #14614, #5135, #4136 ) ;
#6754=CARTESIAN_POINT ( 'NONE',  ( -15.49969986081099904, 10.68321993080349763, 24.21206422150099868 ) ) ;
#6756=CARTESIAN_POINT ( 'NONE',  ( -17.75434499014690104, -17.41303747754496811, -13.22090772388956914 ) ) ;
#6757=ORIENTED_EDGE ( 'NONE', *, *, #14408, .T. ) ;
#6758=ORIENTED_EDGE ( 'NONE', *, *, #5067, .T. ) ;
#6767=AXIS2_PLACEMENT_3D ( 'NONE', #4178, #8831, #13515 ) ;
#6769=VECTOR ( 'NONE', #14508, 1000.000000000000000 ) ;
#6780=DIRECTION ( 'NONE',  ( 0.000000000000000000, -1.225619847157526848E-16, 1.000000000000000000 ) ) ;
#6789=AXIS2_PLACEMENT_3D ( 'NONE', #4381, #12419, #6809 ) ;
#6795=CARTESIAN_POINT ( 'NONE',  ( 15.62304162684920428, -29.63692282015450985, 45.13253465925490815 ) ) ;
#6809=DIRECTION ( 'NONE',  ( 1.000000000000000000, 0.000000000000000000, 0.000000000000000000 ) ) ;
#6814=FACE_BOUND ( 'NONE', #722, .T. ) ;
#6816=CARTESIAN_POINT ( 'NONE',  ( 14.77462936471488142, -26.10186736074272673, 46.34164862513579664 ) ) ;
#6825=ORIENTED_EDGE ( 'NONE', *, *, #5500, .F. ) ;
#6829=DIRECTION ( 'NONE',  ( 0.000000000000000000, -2.168404344971008868E-16, 1.000000000000000000 ) ) ;
#6853=CARTESIAN_POINT ( 'NONE',  ( -35.68452948511416167, 6.083222336789435580, 29.65309064885218859 ) ) ;
#6854=DIRECTION ( 'NONE',  ( 1.049727191138615861E-16, 0.5150380749100581523, -0.8571673007021098911 ) ) ;
#6856=LINE ( 'NONE', #14909, #13778 ) ;
#6868=CARTESIAN_POINT ( 'NONE',  ( -2.216578225681298697, -31.14135358865360104, -10.85656391856669778 ) ) ;
#6879=CIRCLE ( 'NONE', #5187, 22.99999999999999645 ) ;
#6884=AXIS2_PLACEMENT_3D ( 'NONE', #1249, #5904, #265 ) ;
#6885=AXIS2_PLACEMENT_3D ( 'NONE', #1393, #2469, #11798 ) ;
#6887=EDGE_CURVE ( 'NONE', #1247, #14370, #12724, .T. ) ;
#6888=VERTEX_POINT ( 'NONE', #2006 ) ;
#6900=DIRECTION ( 'NONE',  ( 0.000000000000000000, 1.000000000000000000, 1.224646799147350002E-16 ) ) ;
#6902=ADVANCED_FACE ( 'NONE', ( #9343 ), #249, .T. ) ;
#6903=LINE ( 'NONE', #2029, #837 ) ;
#6905=DIRECTION ( 'NONE',  ( 0.000000000000000000, 0.000000000000000000, 1.000000000000000000 ) ) ;
#6912=VECTOR ( 'NONE', #12853, 1000.000000000000000 ) ;
#6925=CARTESIAN_POINT ( 'NONE',  ( -35.90391930765986928, 5.977956585851525340, 29.53688810851901181 ) ) ;
#6937=FACE_BOUND ( 'NONE', #13453, .T. ) ;
#6939=CARTESIAN_POINT ( 'NONE',  ( 14.68618260102866913, -27.00737899243800300, 1.962064221501000683 ) ) ;
#6942=ORIENTED_EDGE ( 'NONE', *, *, #10633, .F. ) ;
#6945=CARTESIAN_POINT ( 'NONE',  ( -22.10635852801940260, -5.970339595447221370, 61.12849997418209114 ) ) ;
#6951=EDGE_CURVE ( 'NONE', #9250, #6353, #4533, .T. ) ;
#6954=CARTESIAN_POINT ( 'NONE',  ( 15.03594476211659270, -25.29111237089811581, 2.444031612587182156 ) ) ;
#6976=CARTESIAN_POINT ( 'NONE',  ( -17.49270643681038706, -17.55260497673067732, -13.23591867084377327 ) ) ;
#6978=VERTEX_POINT ( 'NONE', #1155 ) ;
#6981=CIRCLE ( 'NONE', #6018, 23.00000000000000000 ) ;
#6993=CARTESIAN_POINT ( 'NONE',  ( -37.04494295528539993, 20.99262100756200056, 16.16206422150100153 ) ) ;
#6996=CARTESIAN_POINT ( 'NONE',  ( -35.90397664832814684, 5.977929128642675671, 29.53685653062469640 ) ) ;
#6997=PLANE ( 'NONE',  #12814 ) ;
#7012=CARTESIAN_POINT ( 'NONE',  ( 7.000300139189000070, -19.50737899243800300, 24.21206422150099868 ) ) ;
#7015=AXIS2_PLACEMENT_3D ( 'NONE', #200, #5993, #9520 ) ;
#7028=AXIS2_PLACEMENT_3D ( 'NONE', #6437, #13421, #6213 ) ;
#7030=DIRECTION ( 'NONE',  ( 0.000000000000000000, -1.000000000000000000, -1.224646799147350002E-16 ) ) ;
#7039=ORIENTED_EDGE ( 'NONE', *, *, #2981, .F. ) ;
#7042=SURFACE_STYLE_USAGE ( .BOTH. , #258 ) ;
#7051=DIRECTION ( 'NONE',  ( 7.070501591499390115E-17, -1.224646799147350002E-16, 1.000000000000000000 ) ) ;
#7053=CARTESIAN_POINT ( 'NONE',  ( -15.49969986081099904, -32.00737899243799944, 24.21206422150099868 ) ) ;
#7054=EDGE_CURVE ( 'NONE', #11046, #10705, #545, .T. ) ;
#7055=CYLINDRICAL_SURFACE ( 'NONE', #2535, 4.499999999999999112 ) ;
#7056=CARTESIAN_POINT ( 'NONE',  ( -38.36092261288197136, 4.383170266566359885, 26.75226997007207075 ) ) ;
#7057=ORIENTED_EDGE ( 'NONE', *, *, #4943, .F. ) ;
#7065=CARTESIAN_POINT ( 'NONE',  ( -15.49969986081099904, 71.39262100756199914, 15.89786062077516782 ) ) ;
#7074=CARTESIAN_POINT ( 'NONE',  ( -15.49969986081100082, 22.99262100756200411, 8.337064221501000461 ) ) ;
#7087=CARTESIAN_POINT ( 'NONE',  ( -6.405052749715342664, -17.67073240653434496, 60.59267971125725438 ) ) ;
#7088=EDGE_CURVE ( 'NONE', #13469, #13305, #8434, .T. ) ;
#7090=EDGE_CURVE ( 'NONE', #1539, #11046, #9651, .T. ) ;
#7098=CARTESIAN_POINT ( 'NONE',  ( 7.288334046976859604, 4.602115691088532579, 21.08258158336541399 ) ) ;
#7104=FACE_OUTER_BOUND ( 'NONE', #12660, .T. ) ;
#7106=CARTESIAN_POINT ( 'NONE',  ( 0.8003001391889992266, 20.99262100756200056, 16.16206422150100153 ) ) ;
#7118=CARTESIAN_POINT ( 'NONE',  ( -15.49969986081099904, -13.50737899243800122, 6.712064221500998684 ) ) ;
#7125=CYLINDRICAL_SURFACE ( 'NONE', #6884, 2.499999999999998668 ) ;
#7136=DIRECTION ( 'NONE',  ( 0.000000000000000000, 0.000000000000000000, 1.000000000000000000 ) ) ;
#7141=ORIENTED_EDGE ( 'NONE', *, *, #4571, .T. ) ;
#7147=CARTESIAN_POINT ( 'NONE',  ( -15.49969986081099727, 71.39262100756199914, 32.52626782222684909 ) ) ;
#7152=CARTESIAN_POINT ( 'NONE',  ( -23.49969986081099904, -19.50737899243800300, 60.84879442494580104 ) ) ;
#7156=CIRCLE ( 'NONE', #581, 22.99999999999999645 ) ;
#7162=ORIENTED_EDGE ( 'NONE', *, *, #7570, .F. ) ;
#7164=LINE ( 'NONE', #1286, #11926 ) ;
#7168=PLANE ( 'NONE',  #13014 ) ;
#7173=CARTESIAN_POINT ( 'NONE',  ( 18.53245405280430802, -27.00737899243800300, 8.462064221501000461 ) ) ;
#7174=DIRECTION ( 'NONE',  ( 0.000000000000000000, 0.000000000000000000, 1.000000000000000000 ) ) ;
#7176=CIRCLE ( 'NONE', #2794, 2.499999999999998668 ) ;
#7180=ORIENTED_EDGE ( 'NONE', *, *, #6504, .T. ) ;
#7197=VERTEX_POINT ( 'NONE', #11948 ) ;
#7206=EDGE_CURVE ( 'NONE', #2844, #1400, #12321, .T. ) ;
#7209=DIRECTION ( 'NONE',  ( 0.000000000000000000, -1.000000000000000000, -1.224646799147350002E-16 ) ) ;
#7211=CARTESIAN_POINT ( 'NONE',  ( -38.49826176900612751, 3.992621007561997892, 24.89858491813232177 ) ) ;
#7214=CARTESIAN_POINT ( 'NONE',  ( -23.82178639965737688, -19.07793027397611141, 60.77846357673786315 ) ) ;
#7219=ORIENTED_EDGE ( 'NONE', *, *, #93, .T. ) ;
#7235=STYLED_ITEM ( 'NONE', ( #1551 ), #2515 ) ;
#7248=ORIENTED_EDGE ( 'NONE', *, *, #2353, .T. ) ;
#7256=CIRCLE ( 'NONE', #205, 23.00000000000000000 ) ;
#7258=ORIENTED_EDGE ( 'NONE', *, *, #14769, .T. ) ;
#7278=ORIENTED_EDGE ( 'NONE', *, *, #454, .T. ) ;
#7287=CARTESIAN_POINT ( 'NONE',  ( -15.49969986081099904, 64.39262100756199914, 24.21206422150100579 ) ) ;
#7289=CARTESIAN_POINT ( 'NONE',  ( -15.49969986081099904, 12.99262100756199878, 24.21206422150099868 ) ) ;
#7295=CARTESIAN_POINT ( 'NONE',  ( -25.28633754730619643, -15.63094115750824820, 60.41261054227882710 ) ) ;
#7298=CARTESIAN_POINT ( 'NONE',  ( 21.88653531229833860, -28.45002520398911727, 27.13200563053409553 ) ) ;
#7301=CONICAL_SURFACE ( 'NONE', #6561, 6.250000000000001776, 0.7853981633974461696 ) ;
#7314=FACE_OUTER_BOUND ( 'NONE', #1869, .T. ) ;
#7322=EDGE_CURVE ( 'NONE', #14421, #2329, #11693, .T. ) ;
#7325=AXIS2_PLACEMENT_3D ( 'NONE', #8283, #268, #2558 ) ;
#7326=CARTESIAN_POINT ( 'NONE',  ( 18.10049798887294514, -29.26525578417205153, 7.559493535731737879 ) ) ;
#7343=CARTESIAN_POINT ( 'NONE',  ( -2.216578225681298697, -32.00737899243799944, 59.28069236156870403 ) ) ;
#7348=ORIENTED_EDGE ( 'NONE', *, *, #5503, .T. ) ;
#7350=SURFACE_STYLE_FILL_AREA ( #10808 ) ;
#7351=ORIENTED_EDGE ( 'NONE', *, *, #4560, .F. ) ;
#7358=EDGE_CURVE ( 'NONE', #15087, #8216, #8172, .T. ) ;
#7374=EDGE_CURVE ( 'NONE', #5152, #5621, #3872, .T. ) ;
#7379=ADVANCED_FACE ( 'NONE', ( #7529, #7749 ), #8905, .T. ) ;
#7381=EDGE_CURVE ( 'NONE', #1870, #2152, #9906, .T. ) ;
#7384=FACE_OUTER_BOUND ( 'NONE', #5942, .T. ) ;
#7386=ORIENTED_EDGE ( 'NONE', *, *, #2316, .T. ) ;
#7390=ORIENTED_EDGE ( 'NONE', *, *, #6521, .T. ) ;
#7403=AXIS2_PLACEMENT_3D ( 'NONE', #12213, #4330, #7683 ) ;
#7404=CARTESIAN_POINT ( 'NONE',  ( 16.32110505353168861, -30.15237131756928690, 4.369237647224089471 ) ) ;
#7419=CARTESIAN_POINT ( 'NONE',  ( -32.76014075162859740, 10.68321993080349763, 16.26994987741149856 ) ) ;
#7423=CARTESIAN_POINT ( 'NONE',  ( -15.49969986081099904, 70.89785811302749607, 24.21206422150100579 ) ) ;
#7433=ORIENTED_EDGE ( 'NONE', *, *, #3047, .F. ) ;
#7434=EDGE_CURVE ( 'NONE', #14532, #14421, #13360, .T. ) ;
#7437=CARTESIAN_POINT ( 'NONE',  ( -15.49969986081099904, 22.99262100756200056, 24.21206422150099868 ) ) ;
#7442=CARTESIAN_POINT ( 'NONE',  ( -35.92581786978435332, 5.967462257416473292, 18.89919563306356665 ) ) ;
#7451=VERTEX_POINT ( 'NONE', #6372 ) ;
#7452=EDGE_CURVE ( 'NONE', #970, #3001, #14039, .T. ) ;
#7453=CARTESIAN_POINT ( 'NONE',  ( 2.374542637206501272, 7.183219930803497633, 17.76912582958182085 ) ) ;
#7457=FACE_BOUND ( 'NONE', #12182, .T. ) ;
#7465=CARTESIAN_POINT ( 'NONE',  ( 21.97317718429104616, -24.08580327976269331, 22.77252883434266550 ) ) ;
#7468=AXIS2_PLACEMENT_3D ( 'NONE', #3799, #13069, #4954 ) ;
#7471=CARTESIAN_POINT ( 'NONE',  ( -15.49969986081099904, 20.99262100756200056, 24.21206422150099868 ) ) ;
#7476=CARTESIAN_POINT ( 'NONE',  ( 18.35413756676371122, -28.54901284085133639, 8.082023903208540361 ) ) ;
#7481=EDGE_LOOP ( 'NONE', ( #6072, #1303 ) ) ;
#7483=ADVANCED_FACE ( 'NONE', ( #11358 ), #881, .F. ) ;
#7484=ORIENTED_EDGE ( 'NONE', *, *, #6093, .F. ) ;
#7485=DIRECTION ( 'NONE',  ( 0.000000000000000000, 1.000000000000000000, 1.224646799147350002E-16 ) ) ;
#7501=DIRECTION ( 'NONE',  ( 0.000000000000000000, -0.4999999999999993339, -0.8660254037844390407 ) ) ;
#7505=ORIENTED_EDGE ( 'NONE', *, *, #11751, .T. ) ;
#7529=FACE_OUTER_BOUND ( 'NONE', #2546, .T. ) ;
#7530=CARTESIAN_POINT ( 'NONE',  ( 5.426450521646303926, 12.65779542994540208, 32.26206422150099939 ) ) ;
#7540=CARTESIAN_POINT ( 'NONE',  ( 21.85920135429434907, -27.00737899243800300, 20.96206422150100224 ) ) ;
#7541=FACE_OUTER_BOUND ( 'NONE', #5529, .T. ) ;
#7546=FACE_OUTER_BOUND ( 'NONE', #6048, .T. ) ;
#7552=CARTESIAN_POINT ( 'NONE',  ( 0.8003001391889992266, 20.99262100756200056, 24.21206422150100224 ) ) ;
#7554=EDGE_LOOP ( 'NONE', ( #8046, #10335, #5108, #763 ) ) ;
#7560=EDGE_LOOP ( 'NONE', ( #8067, #11976 ) ) ;
#7561=ADVANCED_FACE ( 'NONE', ( #1251 ), #9668, .F. ) ;
#7562=ORIENTED_EDGE ( 'NONE', *, *, #14148, .F. ) ;
#7563=AXIS2_PLACEMENT_3D ( 'NONE', #6595, #7678, #12359 ) ;
#7569=DIRECTION ( 'NONE',  ( 0.000000000000000000, 1.000000000000000000, 1.224646799147350002E-16 ) ) ;
#7570=EDGE_CURVE ( 'NONE', #11046, #9250, #2696, .T. ) ;
#7574=FACE_OUTER_BOUND ( 'NONE', #14099, .T. ) ;
#7580=DIRECTION ( 'NONE',  ( 0.000000000000000000, -1.000000000000000000, -1.224646799147350002E-16 ) ) ;
#7592=EDGE_CURVE ( 'NONE', #2975, #11290, #120, .T. ) ;
#7602=EDGE_LOOP ( 'NONE', ( #4449, #10116, #13851 ) ) ;
#7606=DIRECTION ( 'NONE',  ( 0.000000000000000000, 1.000000000000000000, 1.224646799147350002E-16 ) ) ;
#7614=ORIENTED_EDGE ( 'NONE', *, *, #11117, .T. ) ;
#7621=PLANE ( 'NONE',  #9269 ) ;
#7627=DIRECTION ( 'NONE',  ( -1.000000000000000000, 0.000000000000000000, 0.000000000000000000 ) ) ;
#7630=CARTESIAN_POINT ( 'NONE',  ( -15.49969986081099904, -32.00737899243799944, 24.21206422150100224 ) ) ;
#7634=DIRECTION ( 'NONE',  ( 0.000000000000000000, 0.000000000000000000, 1.000000000000000000 ) ) ;
#7641=DIRECTION ( 'NONE',  ( 0.000000000000000000, 0.000000000000000000, -1.000000000000000000 ) ) ;
#7648=EDGE_LOOP ( 'NONE', ( #8511, #9990 ) ) ;
#7653=EDGE_CURVE ( 'NONE', #2329, #1607, #13218, .T. ) ;
#7658=CARTESIAN_POINT ( 'NONE',  ( -11.23011178639221086, -12.05596824276080348, -13.04425562498458291 ) ) ;
#7659=ADVANCED_FACE ( 'NONE', ( #3005 ), #563, .T. ) ;
#7662=EDGE_CURVE ( 'NONE', #1400, #9211, #14664, .T. ) ;
#7668=CARTESIAN_POINT ( 'NONE',  ( -25.49893968439952729, -13.50738396921345519, 60.35575980305132049 ) ) ;
#7678=DIRECTION ( 'NONE',  ( 0.8660254037844387076, -0.4999999999999998890, 0.000000000000000000 ) ) ;
#7682=DIRECTION ( 'NONE',  ( 0.000000000000000000, 1.131341397376178572E-16, -1.000000000000000000 ) ) ;
#7683=DIRECTION ( 'NONE',  ( -7.070501591499349439E-17, 0.000000000000000000, 1.000000000000000000 ) ) ;
#7693=PRODUCT_CONTEXT ( 'NONE', #13111, 'mechanical' ) ;
#7711=FACE_BOUND ( 'NONE', #6685, .T. ) ;
#7715=DIRECTION ( 'NONE',  ( 0.000000000000000000, -2.220446049250312588E-16, 1.000000000000000000 ) ) ;
#7724=ORIENTED_EDGE ( 'NONE', *, *, #2453, .T. ) ;
#7730=CIRCLE ( 'NONE', #12399, 2.500000000000002220 ) ;
#7736=EDGE_CURVE ( 'NONE', #1870, #3162, #1231, .T. ) ;
#7740=CARTESIAN_POINT ( 'NONE',  ( -15.49969986081099904, 22.99262100756199700, 40.08706422150100224 ) ) ;
#7748=CIRCLE ( 'NONE', #441, 4.999999999999997335 ) ;
#7749=FACE_BOUND ( 'NONE', #381, .T. ) ;
#7758=CARTESIAN_POINT ( 'NONE',  ( 5.018124931134533284, 5.923502402102436726, 29.47442983242405745 ) ) ;
#7760=EDGE_LOOP ( 'NONE', ( #10598, #2790, #12292, #6758, #14349, #9931 ) ) ;
#7761=DIRECTION ( 'NONE',  ( 0.000000000000000000, -1.334178587669858246E-16, 1.000000000000000000 ) ) ;
#7765=CARTESIAN_POINT ( 'NONE',  ( 21.89425379661516047, -25.37906976104908452, 27.03274040250693488 ) ) ;
#7766=DIRECTION ( 'NONE',  ( 1.000000000000000000, -3.922012711866029438E-32, 3.202566417187950042E-16 ) ) ;
#7777=CARTESIAN_POINT ( 'NONE',  ( -33.23380676216500973, 7.699995122771584377, 31.04377206689012425 ) ) ;
#7787=CARTESIAN_POINT ( 'NONE',  ( 7.000300139189000070, -32.00737899243799944, 24.21206422150099868 ) ) ;
#7791=CARTESIAN_POINT ( 'NONE',  ( -38.29214122569165824, 4.584400081984788322, 21.07650941979234815 ) ) ;
#7795=CARTESIAN_POINT ( 'NONE',  ( 17.66550352352905406, -29.89979048896684688, 41.71521872389765662 ) ) ;
#7796=EDGE_LOOP ( 'NONE', ( #3825, #1398, #9696, #1189 ) ) ;
#7797=EDGE_LOOP ( 'NONE', ( #11241, #170, #10789, #2815 ) ) ;
#7801=DIRECTION ( 'NONE',  ( 0.000000000000000000, 0.000000000000000000, -1.000000000000000000 ) ) ;
#7808=CARTESIAN_POINT ( 'NONE',  ( 17.94020077395062174, -24.45836243756893325, 41.18425341717939148 ) ) ;
#7809=VERTEX_POINT ( 'NONE', #10105 ) ;
#7821=CARTESIAN_POINT ( 'NONE',  ( -15.49969986081099904, 20.99262100756200411, 8.587064221501000461 ) ) ;
#7824=ORIENTED_EDGE ( 'NONE', *, *, #1317, .F. ) ;
#7832=ORIENTED_EDGE ( 'NONE', *, *, #4982, .T. ) ;
#7836=CIRCLE ( 'NONE', #2740, 28.00000000000000000 ) ;
#7843=VERTEX_POINT ( 'NONE', #4456 ) ;
#7849=CARTESIAN_POINT ( 'NONE',  ( 7.500245791298697284, 3.992621007561997892, 24.26206422150100295 ) ) ;
#7850=ORIENTED_EDGE ( 'NONE', *, *, #248, .T. ) ;
#7857=DIRECTION ( 'NONE',  ( 3.202566417187950042E-16, 1.224646799147350002E-16, -1.000000000000000000 ) ) ;
#7873=EDGE_LOOP ( 'NONE', ( #11980, #3523, #13488, #6406 ) ) ;
#7877=ORIENTED_EDGE ( 'NONE', *, *, #4982, .F. ) ;
#7889=CARTESIAN_POINT ( 'NONE',  ( 18.53245405280427960, -27.00737899243800300, 39.96206422150099513 ) ) ;
#7894=CARTESIAN_POINT ( 'NONE',  ( -15.49969986081099904, 0.9926210075619987805, 24.21206422150099868 ) ) ;
#7900=LINE ( 'NONE', #4628, #977 ) ;
#7902=FACE_OUTER_BOUND ( 'NONE', #14743, .T. ) ;
#7910=CARTESIAN_POINT ( 'NONE',  ( -18.88797976027533920, -16.48321755670100330, -13.13513021181339013 ) ) ;
#7921=LINE ( 'NONE', #3419, #6323 ) ;
#7924=EDGE_CURVE ( 'NONE', #4803, #2152, #5386, .T. ) ;
#7941=CARTESIAN_POINT ( 'NONE',  ( -6.534518714218351398, -9.065620043482315538, 60.62497794784820826 ) ) ;
#7947=CARTESIAN_POINT ( 'NONE',  ( 16.67206586382257072, -30.25228346699919868, 43.48069578308454908 ) ) ;
#7962=CARTESIAN_POINT ( 'NONE',  ( 14.82713286944436781, -25.88435658361797564, 46.26984121431809172 ) ) ;
#7966=EDGE_LOOP ( 'NONE', ( #1752, #7979, #8241, #14734, #1552 ) ) ;
#7974=CARTESIAN_POINT ( 'NONE',  ( 4.185908152463202470, 11.99262100756819827, 16.16206422150100153 ) ) ;
#7975=CIRCLE ( 'NONE', #6502, 10.00000000000000000 ) ;
#7976=DIRECTION ( 'NONE',  ( -1.000000000000000000, 0.000000000000000000, 0.000000000000000000 ) ) ;
#7978=CARTESIAN_POINT ( 'NONE',  ( 6.018379519091470620, 5.443421374437837024, 28.85885509741335753 ) ) ;
#7979=ORIENTED_EDGE ( 'NONE', *, *, #847, .T. ) ;
#7982=CARTESIAN_POINT ( 'NONE',  ( -19.76919792506910412, -14.95941792723064090, -13.04426848743355549 ) ) ;
#7999=CARTESIAN_POINT ( 'NONE',  ( -28.78282149594069850, -32.00737899243799944, 59.28069236156870403 ) ) ;
#8002=CARTESIAN_POINT ( 'NONE',  ( -34.10510093996977332, 6.837078596115874873, 30.39460083794530121 ) ) ;
#8004=LINE ( 'NONE', #12693, #1446 ) ;
#8008=ORIENTED_EDGE ( 'NONE', *, *, #8188, .F. ) ;
#8009=AXIS2_PLACEMENT_3D ( 'NONE', #1133, #10622, #9399 ) ;
#8016=EDGE_CURVE ( 'NONE', #3237, #1870, #3688, .T. ) ;
#8017=DIRECTION ( 'NONE',  ( -1.000000000000000000, 0.000000000000000000, 0.000000000000000000 ) ) ;
#8025=VECTOR ( 'NONE', #3352, 1000.000000000000000 ) ;
#8027=ORIENTED_EDGE ( 'NONE', *, *, #4800, .F. ) ;
#8033=DIRECTION ( 'NONE',  ( 0.000000000000000000, 1.000000000000000000, 1.224646799147350002E-16 ) ) ;
#8037=CIRCLE ( 'NONE', #4140, 37.50000000000000000 ) ;
#8040=PLANE ( 'NONE',  #2764 ) ;
#8042=CARTESIAN_POINT ( 'NONE',  ( -10.99969986081100259, -13.80113588252518397, -13.01695671647156338 ) ) ;
#8043=ORIENTED_EDGE ( 'NONE', *, *, #9667, .T. ) ;
#8046=ORIENTED_EDGE ( 'NONE', *, *, #9157, .F. ) ;
#8047=CARTESIAN_POINT ( 'NONE',  ( -15.49969986081099904, 0.9926210075619987805, 24.21206422150099868 ) ) ;
#8052=FACE_OUTER_BOUND ( 'NONE', #10655, .T. ) ;
#8056=DIRECTION ( 'NONE',  ( 0.000000000000000000, -1.000000000000000000, -1.224646799147350002E-16 ) ) ;
#8061=ORIENTED_EDGE ( 'NONE', *, *, #248, .F. ) ;
#8062=FACE_OUTER_BOUND ( 'NONE', #7554, .T. ) ;
#8067=ORIENTED_EDGE ( 'NONE', *, *, #10669, .F. ) ;
#8072=DIRECTION ( 'NONE',  ( 0.000000000000000000, 1.000000000000000000, 1.224646799147350002E-16 ) ) ;
#8077=EDGE_CURVE ( 'NONE', #1607, #2329, #1487, .T. ) ;
#8093=EDGE_CURVE ( 'NONE', #13514, #1150, #9537, .T. ) ;
#8098=CARTESIAN_POINT ( 'NONE',  ( -19.93511768254584027, -4.540527604665721917, 61.44996334348378753 ) ) ;
#8105=ORIENTED_EDGE ( 'NONE', *, *, #4306, .T. ) ;
#8109=VECTOR ( 'NONE', #7857, 1000.000000000000000 ) ;
#8111=DIRECTION ( 'NONE',  ( 0.000000000000000000, 0.000000000000000000, 1.000000000000000000 ) ) ;
#8118=CARTESIAN_POINT ( 'NONE',  ( -15.20596105127630082, -18.00737899243800655, -13.28793577849899599 ) ) ;
#8123=VERTEX_POINT ( 'NONE', #7343 ) ;
#8124=EDGE_CURVE ( 'NONE', #9649, #1625, #11899, .T. ) ;
#8128=EDGE_CURVE ( 'NONE', #3162, #1870, #5534, .T. ) ;
#8129=AXIS2_PLACEMENT_3D ( 'NONE', #9022, #8944, #5732 ) ;
#8130=CARTESIAN_POINT ( 'NONE',  ( 0.8003001391889992266, 11.99262100756199878, 24.16206422150099442 ) ) ;
#8135=LINE ( 'NONE', #10516, #12682 ) ;
#8146=ORIENTED_EDGE ( 'NONE', *, *, #14356, .F. ) ;
#8160=CIRCLE ( 'NONE', #10109, 2.500000000000000444 ) ;
#8170=EDGE_CURVE ( 'NONE', #11942, #9206, #10031, .T. ) ;
#8172=CIRCLE ( 'NONE', #13080, 2.500000000000000444 ) ;
#8179=PRODUCT_DEFINITION_CONTEXT ( 'detailed design', #14753, 'design' ) ;
#8180=EDGE_LOOP ( 'NONE', ( #7850, #1775, #8480, #10672 ) ) ;
#8188=EDGE_CURVE ( 'NONE', #1150, #13514, #5300, .T. ) ;
#8191=CARTESIAN_POINT ( 'NONE',  ( -19.85426396466228027, -12.33449077490513623, -13.03429394648231643 ) ) ;
#8195=ORIENTED_EDGE ( 'NONE', *, *, #11717, .F. ) ;
#8197=ORIENTED_EDGE ( 'NONE', *, *, #849, .F. ) ;
#8198=AXIS2_PLACEMENT_3D ( 'NONE', #1755, #9795, #5273 ) ;
#8205=EDGE_CURVE ( 'NONE', #10768, #5054, #10161, .T. ) ;
#8206=DIRECTION ( 'NONE',  ( 0.000000000000000000, -1.000000000000000000, -1.224646799147350002E-16 ) ) ;
#8210=PLANE ( 'NONE',  #122 ) ;
#8213=ORIENTED_EDGE ( 'NONE', *, *, #13794, .T. ) ;
#8216=VERTEX_POINT ( 'NONE', #12706 ) ;
#8219=CARTESIAN_POINT ( 'NONE',  ( 21.85920135429435263, -27.00737899243800300, 27.46206422150099868 ) ) ;
#8231=CIRCLE ( 'NONE', #10440, 3.249999999999999556 ) ;
#8233=LINE ( 'NONE', #7999, #13550 ) ;
#8235=DIRECTION ( 'NONE',  ( 3.632077277826439854E-16, -1.000000000000000000, 0.000000000000000000 ) ) ;
#8241=ORIENTED_EDGE ( 'NONE', *, *, #6368, .T. ) ;
#8245=VECTOR ( 'NONE', #10380, 1000.000000000000000 ) ;
#8249=FACE_OUTER_BOUND ( 'NONE', #89, .T. ) ;
#8270=FACE_OUTER_BOUND ( 'NONE', #7796, .T. ) ;
#8280=CARTESIAN_POINT ( 'NONE',  ( -15.49969986081099904, 4.873818854045000037, 24.21206422150099868 ) ) ;
#8281=CIRCLE ( 'NONE', #1691, 8.000000000000000000 ) ;
#8283=CARTESIAN_POINT ( 'NONE',  ( 0.8003001391889992266, 20.99262100756200056, 16.16206422150100153 ) ) ;
#8284=FACE_OUTER_BOUND ( 'NONE', #377, .T. ) ;
#8287=CARTESIAN_POINT ( 'NONE',  ( -15.49969986081099904, 13.89262100756199736, 24.21206422150099868 ) ) ;
#8288=EDGE_LOOP ( 'NONE', ( #13962, #9488 ) ) ;
#8292=AXIS2_PLACEMENT_3D ( 'NONE', #8752, #7606, #1955 ) ;
#8307=CARTESIAN_POINT ( 'NONE',  ( 2.377116011596429601, -23.18484177525208167, 57.27215087687874018 ) ) ;
#8310=ADVANCED_FACE ( 'NONE', ( #7711, #12941, #6937, #5950 ), #10476, .T. ) ;
#8311=CARTESIAN_POINT ( 'NONE',  ( 9.000300139189000959, -27.00737899243800300, 21.71206422150100224 ) ) ;
#8317=EDGE_CURVE ( 'NONE', #9206, #6888, #4035, .T. ) ;
#8321=CARTESIAN_POINT ( 'NONE',  ( -15.49969986081099904, 13.89262100756199736, 24.21206422150099868 ) ) ;
#8323=CARTESIAN_POINT ( 'NONE',  ( 14.82707475067032199, -28.13046415553212043, 2.154202982575026404 ) ) ;
#8329=VERTEX_POINT ( 'NONE', #10626 ) ;
#8346=CARTESIAN_POINT ( 'NONE',  ( 18.53245405280430091, -26.77391037161654808, 8.462064221500996908 ) ) ;
#8360=DIRECTION ( 'NONE',  ( 0.000000000000000000, 0.000000000000000000, 1.000000000000000000 ) ) ;
#8366=CARTESIAN_POINT ( 'NONE',  ( -36.42585024326910315, 12.65779542994580353, 32.26206422150099939 ) ) ;
#8369=DIRECTION ( 'NONE',  ( 0.000000000000000000, 0.000000000000000000, 1.000000000000000000 ) ) ;
#8378=FACE_OUTER_BOUND ( 'NONE', #14270, .T. ) ;
#8388=ORIENTED_EDGE ( 'NONE', *, *, #13296, .T. ) ;
#8389=PLANE ( 'NONE',  #11953 ) ;
#8393=ORIENTED_EDGE ( 'NONE', *, *, #1369, .T. ) ;
#8394=DIRECTION ( 'NONE',  ( 0.000000000000000000, -1.000000000000000000, -1.224646799147350002E-16 ) ) ;
#8398=CARTESIAN_POINT ( 'NONE',  ( -15.49969986081099904, 70.81438635534659909, 30.46206422150100934 ) ) ;
#8406=LINE ( 'NONE', #5122, #2640 ) ;
#8407=VECTOR ( 'NONE', #8072, 1000.000000000000000 ) ;
#8416=FACE_OUTER_BOUND ( 'NONE', #7760, .T. ) ;
#8418=CARTESIAN_POINT ( 'NONE',  ( 22.00030013918900096, -27.00737899243800300, 20.96206422150100224 ) ) ;
#8425=CARTESIAN_POINT ( 'NONE',  ( 18.44214592757203519, -25.87850161324475451, 8.268049333039575899 ) ) ;
#8434=CIRCLE ( 'NONE', #1839, 22.99999999999999645 ) ;
#8435=LINE ( 'NONE', #6124, #3227 ) ;
#8437=CARTESIAN_POINT ( 'NONE',  ( -15.49969986081099904, 10.68321993080349763, 24.21206422150099868 ) ) ;
#8442=VECTOR ( 'NONE', #5634, 1000.000000000000000 ) ;
#8447=CARTESIAN_POINT ( 'NONE',  ( -15.49969986081099904, 64.39262100756199914, 17.96206422150100579 ) ) ;
#8449=ORIENTED_EDGE ( 'NONE', *, *, #13236, .T. ) ;
#8451=CARTESIAN_POINT ( 'NONE',  ( 21.89421144759936766, -28.63483922330976483, 21.39079340381945471 ) ) ;
#8457=AXIS2_PLACEMENT_3D ( 'NONE', #1992, #6714, #10248 ) ;
#8459=DIRECTION ( 'NONE',  ( 0.000000000000000000, -1.000000000000000000, -1.224646799147350002E-16 ) ) ;
#8461=DIRECTION ( 'NONE',  ( 1.000000000000000000, 3.700743415417188632E-16, 0.000000000000000000 ) ) ;
#8462=EDGE_LOOP ( 'NONE', ( #1492, #7248, #5156, #4224 ) ) ;
#8464=VECTOR ( 'NONE', #8017, 1000.000000000000000 ) ;
#8469=DIRECTION ( 'NONE',  ( -1.000000000000000000, 0.000000000000000000, 0.000000000000000000 ) ) ;
#8473=ADVANCED_FACE ( 'NONE', ( #2821 ), #13139, .T. ) ;
#8477=DIRECTION ( 'NONE',  ( -1.000000000000000000, 0.000000000000000000, 0.000000000000000000 ) ) ;
#8478=AXIS2_PLACEMENT_3D ( 'NONE', #220, #296, #14214 ) ;
#8480=ORIENTED_EDGE ( 'NONE', *, *, #2519, .T. ) ;
#8490=EDGE_CURVE ( 'NONE', #10768, #11542, #12636, .T. ) ;
#8501=VECTOR ( 'NONE', #14730, 1000.000000000000000 ) ;
#8502=CARTESIAN_POINT ( 'NONE',  ( -15.49969986081099904, 3.992621007561997892, 24.21206422150099868 ) ) ;
#8503=CARTESIAN_POINT ( 'NONE',  ( -15.49969986081099904, 10.68321993080349763, 24.21206422150099868 ) ) ;
#8505=DIRECTION ( 'NONE',  ( 0.000000000000000000, 0.000000000000000000, 1.000000000000000000 ) ) ;
#8507=ORIENTED_EDGE ( 'NONE', *, *, #562, .T. ) ;
#8511=ORIENTED_EDGE ( 'NONE', *, *, #3027, .F. ) ;
#8517=DIRECTION ( 'NONE',  ( 0.000000000000000000, 0.000000000000000000, 1.000000000000000000 ) ) ;
#8530=CARTESIAN_POINT ( 'NONE',  ( -15.49969986081099727, 22.99262100756199700, 39.83706422150100224 ) ) ;
#8534=CARTESIAN_POINT ( 'NONE',  ( 3.243537350957551357, 11.48902252484887399, 32.26206422150129072 ) ) ;
#8537=EDGE_CURVE ( 'NONE', #9493, #5899, #6981, .T. ) ;
#8540=ORIENTED_EDGE ( 'NONE', *, *, #7088, .T. ) ;
#8550=DIRECTION ( 'NONE',  ( -1.000000000000000000, 0.000000000000000000, 0.000000000000000000 ) ) ;
#8554=CARTESIAN_POINT ( 'NONE',  ( 16.90967644101677081, -30.26063172738379237, 5.345825581268424997 ) ) ;
#8556=VERTEX_POINT ( 'NONE', #5486 ) ;
#8568=CARTESIAN_POINT ( 'NONE',  ( -11.65397503470588703, -4.262226922354281911, 61.51805161050018711 ) ) ;
#8570=DIRECTION ( 'NONE',  ( 0.000000000000000000, -1.000000000000000000, -1.224646799147350002E-16 ) ) ;
#8574=ADVANCED_FACE ( 'NONE', ( #6547 ), #9074, .F. ) ;
#8578=VERTEX_POINT ( 'NONE', #5406 ) ;
#8582=CONICAL_SURFACE ( 'NONE', #5888, 19.00000000000000000, 1.047197551196598297 ) ;
#8595=VERTEX_POINT ( 'NONE', #12609 ) ;
#8598=CARTESIAN_POINT ( 'NONE',  ( -15.49969986081099904, 71.39262100756199914, 31.04029887371640939 ) ) ;
#8600=EDGE_LOOP ( 'NONE', ( #3713, #1700 ) ) ;
#8621=CARTESIAN_POINT ( 'NONE',  ( 21.86106836617108939, -26.57972102403619630, 20.98332789618103078 ) ) ;
#8623=VERTEX_POINT ( 'NONE', #2599 ) ;
#8629=AXIS2_PLACEMENT_3D ( 'NONE', #7630, #5269, #12313 ) ;
#8632=CARTESIAN_POINT ( 'NONE',  ( 18.47602945437533251, -27.91681196510473484, 8.340622674467514486 ) ) ;
#8634=ORIENTED_EDGE ( 'NONE', *, *, #5168, .F. ) ;
#8635=CARTESIAN_POINT ( 'NONE',  ( 13.85920135429429934, -27.00737899243800300, 24.21206422150099868 ) ) ;
#8647=CARTESIAN_POINT ( 'NONE',  ( -10.20730426669924995, -5.016324734929597184, 61.33773678374165428 ) ) ;
#8656=ORIENTED_EDGE ( 'NONE', *, *, #2164, .T. ) ;
#8659=EDGE_LOOP ( 'NONE', ( #13062, #10594 ) ) ;
#8660=CARTESIAN_POINT ( 'NONE',  ( -11.02821192705052233, -12.92121384215898416, -13.02043737883916208 ) ) ;
#8661=AXIS2_PLACEMENT_3D ( 'NONE', #8824, #12433, #730 ) ;
#8665=AXIS2_PLACEMENT_3D ( 'NONE', #11867, #7030, #3608 ) ;
#8666=DIRECTION ( 'NONE',  ( 1.224646799147350002E-16, 1.224646799147350002E-16, -1.000000000000000000 ) ) ;
#8668=LINE ( 'NONE', #1712, #453 ) ;
#8676=EDGE_CURVE ( 'NONE', #14647, #7451, #7730, .T. ) ;
#8683=ORIENTED_EDGE ( 'NONE', *, *, #4586, .T. ) ;
#8689=CARTESIAN_POINT ( 'NONE',  ( 21.85920135429435973, -26.79253637162340596, 27.46206422150100224 ) ) ;
#8717=AXIS2_PLACEMENT_3D ( 'NONE', #14643, #9827, #12199 ) ;
#8720=CARTESIAN_POINT ( 'NONE',  ( -15.49969986081099549, 4.873818854045002702, 1.212064221501000461 ) ) ;
#8726=DIRECTION ( 'NONE',  ( 0.000000000000000000, 1.000000000000000000, 1.224646799147350002E-16 ) ) ;
#8728=ORIENTED_EDGE ( 'NONE', *, *, #3027, .T. ) ;
#8730=DIRECTION ( 'NONE',  ( 0.000000000000000000, -1.000000000000000000, -1.224646799147350002E-16 ) ) ;
#8745=CARTESIAN_POINT ( 'NONE',  ( -15.49969986081099727, 20.99262100756200056, 16.16206422150100153 ) ) ;
#8748=ORIENTED_EDGE ( 'NONE', *, *, #10435, .T. ) ;
#8750=( GEOMETRIC_REPRESENTATION_CONTEXT ( 3 ) GLOBAL_UNCERTAINTY_ASSIGNED_CONTEXT ( ( #14159 ) ) GLOBAL_UNIT_ASSIGNED_CONTEXT ( ( #9265, #11490, #3234 ) ) REPRESENTATION_CONTEXT ( 'NONE', 'WORKASPACE' ) );
#8751=CARTESIAN_POINT ( 'NONE',  ( 4.905497514832876327, 5.977487861575268013, 18.88777277397837651 ) ) ;
#8752=CARTESIAN_POINT ( 'NONE',  ( -15.49969986081099904, 22.99262100756200056, 24.21206422150100224 ) ) ;
#8756=DIRECTION ( 'NONE',  ( 0.000000000000000000, -1.000000000000000000, -1.224646799147350002E-16 ) ) ;
#8763=ORIENTED_EDGE ( 'NONE', *, *, #3385, .T. ) ;
#8765=CARTESIAN_POINT ( 'NONE',  ( 21.94819177811133315, -24.42452669754511874, 26.19626277716416496 ) ) ;
#8770=DIRECTION ( 'NONE',  ( 0.000000000000000000, 1.000000000000000000, 1.224646799147350002E-16 ) ) ;
#8777=CARTESIAN_POINT ( 'NONE',  ( -2.216578225681298697, -31.14135358865360104, -10.85656391856669778 ) ) ;
#8782=ORIENTED_EDGE ( 'NONE', *, *, #2335, .F. ) ;
#8789=EDGE_CURVE ( 'NONE', #12994, #1380, #8231, .T. ) ;
#8790=LINE ( 'NONE', #7787, #8109 ) ;
#8793=DIRECTION ( 'NONE',  ( 0.000000000000000000, 1.000000000000000000, 1.224646799147350002E-16 ) ) ;
#8795=EDGE_CURVE ( 'NONE', #2212, #1827, #4188, .T. ) ;
#8798=ORIENTED_EDGE ( 'NONE', *, *, #5067, .F. ) ;
#8801=VERTEX_POINT ( 'NONE', #676 ) ;
#8805=VERTEX_POINT ( 'NONE', #528 ) ;
#8815=ORIENTED_EDGE ( 'NONE', *, *, #2316, .F. ) ;
#8816=DIRECTION ( 'NONE',  ( 0.000000000000000000, 1.224646799147350002E-16, -1.000000000000000000 ) ) ;
#8823=EDGE_CURVE ( 'NONE', #14257, #14381, #4832, .T. ) ;
#8824=CARTESIAN_POINT ( 'NONE',  ( 13.85920135429429934, -23.75737899243800300, 5.212064221501000461 ) ) ;
#8826=VECTOR ( 'NONE', #5138, 1000.000000000000000 ) ;
#8827=CARTESIAN_POINT ( 'NONE',  ( 17.85205907671969783, -24.33051221079297477, 7.067054605798079869 ) ) ;
#8828=CARTESIAN_POINT ( 'NONE',  ( -15.49969986081099904, 4.873818854045000037, 24.21206422150099868 ) ) ;
#8830=EDGE_LOOP ( 'NONE', ( #11787, #3462, #10611, #3353 ) ) ;
#8831=DIRECTION ( 'NONE',  ( 0.000000000000000000, 1.000000000000000000, 1.224646799147350002E-16 ) ) ;
#8834=CARTESIAN_POINT ( 'NONE',  ( 2.112638720354275801, 8.260196310773689987, 31.34027865485604991 ) ) ;
#8836=CARTESIAN_POINT ( 'NONE',  ( 21.93904460677752510, -24.55902234006768126, 26.35984492706892013 ) ) ;
#8862=CIRCLE ( 'NONE', #8129, 19.00000000000000000 ) ;
#8866=ADVANCED_FACE ( 'NONE', ( #14905 ), #4501, .F. ) ;
#8869=CARTESIAN_POINT ( 'NONE',  ( -8.893080693810389903, -5.970021046718354540, 61.12850859281176952 ) ) ;
#8879=VERTEX_POINT ( 'NONE', #12924 ) ;
#8880=ORIENTED_EDGE ( 'NONE', *, *, #6521, .F. ) ;
#8882=CARTESIAN_POINT ( 'NONE',  ( 1.986653357079260385, 8.906201437978330304, 16.78046892755867958 ) ) ;
#8885=CONICAL_SURFACE ( 'NONE', #2298, 23.00000000000000000, 1.047197551196598297 ) ;
#8886=CARTESIAN_POINT ( 'NONE',  ( -10.99969986081100082, -13.21348903481619708, -13.01695671647156516 ) ) ;
#8889=CARTESIAN_POINT ( 'NONE',  ( 0.8003001391889992266, 3.992621007561997892, 24.21206422150099868 ) ) ;
#8899=ORIENTED_EDGE ( 'NONE', *, *, #2335, .T. ) ;
#8902=DIRECTION ( 'NONE',  ( 0.000000000000000000, 1.000000000000000000, 1.224646799147350002E-16 ) ) ;
#8904=LINE ( 'NONE', #14501, #13275 ) ;
#8905=PLANE ( 'NONE',  #8661 ) ;
#8913=CARTESIAN_POINT ( 'NONE',  ( -15.49969986081099904, 70.81438635534659909, 30.46206422150100934 ) ) ;
#8916=CARTESIAN_POINT ( 'NONE',  ( 2.068939505948752977, 8.472784761962648403, 31.44700642079416397 ) ) ;
#8921=EDGE_LOOP ( 'NONE', ( #15012, #14923 ) ) ;
#8934=FACE_OUTER_BOUND ( 'NONE', #4385, .T. ) ;
#8935=ORIENTED_EDGE ( 'NONE', *, *, #1220, .T. ) ;
#8944=DIRECTION ( 'NONE',  ( 0.000000000000000000, -1.000000000000000000, -1.224646799147350002E-16 ) ) ;
#8945=EDGE_CURVE ( 'NONE', #2643, #6888, #13145, .T. ) ;
#8948=EDGE_LOOP ( 'NONE', ( #8507, #8880, #7258, #10658, #7162, #2958, #12661 ) ) ;
#8951=EDGE_CURVE ( 'NONE', #2643, #3542, #324, .T. ) ;
#8956=DIRECTION ( 'NONE',  ( 0.000000000000000000, 1.131341397376178572E-16, -1.000000000000000000 ) ) ;
#8959=CIRCLE ( 'NONE', #2140, 10.00000000000000000 ) ;
#8960=EDGE_CURVE ( 'NONE', #3429, #8879, #8959, .T. ) ;
#8965=DIRECTION ( 'NONE',  ( -1.000000000000000000, 0.000000000000000000, -0.000000000000000000 ) ) ;
#8970=DIRECTION ( 'NONE',  ( 0.000000000000000000, 1.000000000000000000, 1.224646799147350002E-16 ) ) ;
#8976=DIRECTION ( 'NONE',  ( -1.224646799147350002E-16, -1.224646799147350002E-16, 1.000000000000000000 ) ) ;
#8979=FACE_OUTER_BOUND ( 'NONE', #7648, .T. ) ;
#8996=CARTESIAN_POINT ( 'NONE',  ( -37.04494295528539993, 0.9926210075619987805, 16.16206422150100153 ) ) ;
#9009=DIRECTION ( 'NONE',  ( 0.000000000000000000, -1.000000000000000000, -1.224646799147350002E-16 ) ) ;
#9012=DIRECTION ( 'NONE',  ( 0.000000000000000000, 0.000000000000000000, 1.000000000000000000 ) ) ;
#9018=CARTESIAN_POINT ( 'NONE',  ( -15.49969986081099904, -13.50737899243800122, 6.712064221500998684 ) ) ;
#9020=DIRECTION ( 'NONE',  ( 0.000000000000000000, 0.000000000000000000, 1.000000000000000000 ) ) ;
#9022=CARTESIAN_POINT ( 'NONE',  ( -15.49969986081099904, 7.183219930803497633, 24.21206422150099868 ) ) ;
#9024=DIRECTION ( 'NONE',  ( 0.000000000000000000, -1.000000000000000000, -1.224646799147350002E-16 ) ) ;
#9026=CARTESIAN_POINT ( 'NONE',  ( -24.97954105023504212, -10.26796402423269150, 60.49496404811991113 ) ) ;
#9029=ORIENTED_EDGE ( 'NONE', *, *, #11717, .T. ) ;
#9033=LINE ( 'NONE', #5442, #10738 ) ;
#9038=EDGE_LOOP ( 'NONE', ( #7141, #13837 ) ) ;
#9041=EDGE_LOOP ( 'NONE', ( #14309, #4834 ) ) ;
#9042=CARTESIAN_POINT ( 'NONE',  ( 15.21167767729446396, -24.94319804950077923, 45.73146187706110055 ) ) ;
#9044=CARTESIAN_POINT ( 'NONE',  ( -28.78282149594069850, -31.14135358865360104, -10.85656391856669778 ) ) ;
#9045=VERTEX_POINT ( 'NONE', #13593 ) ;
#9048=ORIENTED_EDGE ( 'NONE', *, *, #12913, .F. ) ;
#9050=ADVANCED_FACE ( 'NONE', ( #5395 ), #14835, .F. ) ;
#9053=CARTESIAN_POINT ( 'NONE',  ( 16.31544005195547342, -23.84671352473236183, 4.356601776764517986 ) ) ;
#9054=EDGE_CURVE ( 'NONE', #4606, #14257, #5487, .T. ) ;
#9059=B_SPLINE_CURVE_WITH_KNOTS ( 'NONE', 3,
 ( #2184, #6680, #14883, #7978, #10052, #13888, #13664, #3099, #7758, #5470, #4407, #12511, #3329, #12440, #4331, #12669, #12596, #887, #3405, #5693 ),
 .UNSPECIFIED., .F., .F.,
 ( 4, 2, 2, 1, 1, 1, 1, 1, 1, 2, 2, 2, 4 ),
 ( 0.000000000000000000, 0.2499999999999539257, 0.3749999999999315548, 0.4374999999999203415, 0.4687499999999145128, 0.4843749999999112377, 0.4921874999999091838, 0.4960937499999086286, 0.4980468749999080735, 0.4990234374999077405, 0.4999999999999074074, 0.7499999999999538147, 1.000000000000000000 ),
 .UNSPECIFIED. ) ;
#9062=FACE_OUTER_BOUND ( 'NONE', #5791, .T. ) ;
#9066=CYLINDRICAL_SURFACE ( 'NONE', #3239, 2.500000000000000444 ) ;
#9068=CARTESIAN_POINT ( 'NONE',  ( -15.49969986081100082, 20.99262100756200056, 32.26206422150099939 ) ) ;
#9071=AXIS2_PLACEMENT_3D ( 'NONE', #2241, #8965, #5452 ) ;
#9074=CYLINDRICAL_SURFACE ( 'NONE', #6507, 4.499999999999999112 ) ;
#9081=LINE ( 'NONE', #5639, #5951 ) ;
#9084=ORIENTED_EDGE ( 'NONE', *, *, #13662, .F. ) ;
#9100=CARTESIAN_POINT ( 'NONE',  ( 16.31615091610032309, -30.15025373772158446, 44.06283711198566522 ) ) ;
#9103=CARTESIAN_POINT ( 'NONE',  ( -24.46506769706380169, -9.065967042131633846, 60.62493186400067202 ) ) ;
#9132=FACE_OUTER_BOUND ( 'NONE', #11540, .T. ) ;
#9133=DIRECTION ( 'NONE',  ( 0.000000000000000000, 0.000000000000000000, 1.000000000000000000 ) ) ;
#9136=DIRECTION ( 'NONE',  ( 0.000000000000000000, -1.000000000000000000, -1.224646799147350002E-16 ) ) ;
#9139=DIRECTION ( 'NONE',  ( 0.000000000000000000, 2.220446049250313081E-16, -1.000000000000000000 ) ) ;
#9142=DIRECTION ( 'NONE',  ( 1.000000000000000000, 0.000000000000000000, 0.000000000000000000 ) ) ;
#9155=CARTESIAN_POINT ( 'NONE',  ( -38.49964551292070070, 3.992621007561997892, 24.16206422150099442 ) ) ;
#9157=EDGE_CURVE ( 'NONE', #12884, #609, #5554, .T. ) ;
#9158=CARTESIAN_POINT ( 'NONE',  ( 13.85920135429429934, -27.00737899243800300, 5.212064221501000461 ) ) ;
#9160=ORIENTED_EDGE ( 'NONE', *, *, #12366, .T. ) ;
#9173=CARTESIAN_POINT ( 'NONE',  ( 18.53245405280427960, -27.00737899243800300, 39.96206422150099513 ) ) ;
#9175=ORIENTED_EDGE ( 'NONE', *, *, #12720, .T. ) ;
#9177=ORIENTED_EDGE ( 'NONE', *, *, #8317, .T. ) ;
#9179=DIRECTION ( 'NONE',  ( 0.000000000000000000, 1.000000000000000000, 1.224646799147350002E-16 ) ) ;
#9186=ORIENTED_EDGE ( 'NONE', *, *, #8490, .F. ) ;
#9193=AXIS2_PLACEMENT_3D ( 'NONE', #1942, #11200, #10114 ) ;
#9204=DIRECTION ( 'NONE',  ( 0.000000000000000000, 0.000000000000000000, -1.000000000000000000 ) ) ;
#9206=VERTEX_POINT ( 'NONE', #4333 ) ;
#9207=CARTESIAN_POINT ( 'NONE',  ( -15.49969986081099904, 9.919219809770899232, 24.21206422150099868 ) ) ;
#9211=VERTEX_POINT ( 'NONE', #9289 ) ;
#9215=CARTESIAN_POINT ( 'NONE',  ( -15.49969986081099904, -13.50737899243800122, 6.712064221500998684 ) ) ;
#9218=CARTESIAN_POINT ( 'NONE',  ( 13.85920135429429934, -27.00737899243800300, 5.212064221501000461 ) ) ;
#9237=AXIS2_PLACEMENT_3D ( 'NONE', #5914, #5764, #13958 ) ;
#9240=CARTESIAN_POINT ( 'NONE',  ( -15.49969986081099904, 4.873818854045000037, 24.21206422150099868 ) ) ;
#9242=VECTOR ( 'NONE', #8976, 1000.000000000000000 ) ;
#9243=ADVANCED_FACE ( 'NONE', ( #13960 ), #1174, .T. ) ;
#9250=VERTEX_POINT ( 'NONE', #1040 ) ;
#9255=CARTESIAN_POINT ( 'NONE',  ( -23.02173274162242578, -6.908505027013068123, 60.95052117575047390 ) ) ;
#9260=DIRECTION ( 'NONE',  ( 0.000000000000000000, -1.225619847157526848E-16, 1.000000000000000000 ) ) ;
#9262=DIRECTION ( 'NONE',  ( 0.000000000000000000, 1.000000000000000000, 1.224646799147350002E-16 ) ) ;
#9265=( LENGTH_UNIT ( ) NAMED_UNIT ( * ) SI_UNIT ( .MILLI., .METRE. ) );
#9269=AXIS2_PLACEMENT_3D ( 'NONE', #3112, #1822, #12228 ) ;
#9272=CARTESIAN_POINT ( 'NONE',  ( -12.10759736803031039, -16.47920669945604288, -13.13479660188859199 ) ) ;
#9276=ORIENTED_EDGE ( 'NONE', *, *, #13201, .T. ) ;
#9278=VERTEX_POINT ( 'NONE', #10365 ) ;
#9281=ADVANCED_FACE ( 'NONE', ( #15031 ), #4555, .T. ) ;
#9286=LINE ( 'NONE', #13957, #13051 ) ;
#9289=CARTESIAN_POINT ( 'NONE',  ( 7.000300139189000070, -19.50737899243800300, 54.21206422150100224 ) ) ;
#9294=AXIS2_PLACEMENT_3D ( 'NONE', #620, #12026, #13401 ) ;
#9311=EDGE_LOOP ( 'NONE', ( #10372, #11554, #6942, #7351 ) ) ;
#9330=CARTESIAN_POINT ( 'NONE',  ( -24.15923398760522645, -8.493147050648126140, 60.69887305834505753 ) ) ;
#9332=VERTEX_POINT ( 'NONE', #8447 ) ;
#9343=FACE_OUTER_BOUND ( 'NONE', #14566, .T. ) ;
#9364=CIRCLE ( 'NONE', #3006, 23.00000000000000000 ) ;
#9371=ORIENTED_EDGE ( 'NONE', *, *, #8170, .T. ) ;
#9373=CARTESIAN_POINT ( 'NONE',  ( -31.79969986081099975, 11.99262100756199878, 24.26206422150100650 ) ) ;
#9377=VECTOR ( 'NONE', #1515, 1000.000000000000000 ) ;
#9379=EDGE_LOOP ( 'NONE', ( #3142, #241, #1172, #7824 ) ) ;
#9381=ORIENTED_EDGE ( 'NONE', *, *, #9809, .F. ) ;
#9383=AXIS2_PLACEMENT_3D ( 'NONE', #8287, #12978, #7136 ) ;
#9384=DIRECTION ( 'NONE',  ( -1.000000000000000000, 0.000000000000000000, 0.000000000000000000 ) ) ;
#9385=VECTOR ( 'NONE', #11003, 1000.000000000000000 ) ;
#9393=ORIENTED_EDGE ( 'NONE', *, *, #12920, .F. ) ;
#9394=FACE_BOUND ( 'NONE', #13352, .T. ) ;
#9399=DIRECTION ( 'NONE',  ( 1.000000000000000000, 0.000000000000000000, 0.000000000000000000 ) ) ;
#9402=CARTESIAN_POINT ( 'NONE',  ( -5.500669204425239656, -13.50739036851649466, 60.35526053768147392 ) ) ;
#9403=VECTOR ( 'NONE', #11414, 1000.000000000000000 ) ;
#9414=EDGE_LOOP ( 'NONE', ( #1925, #4083, #15108, #1589, #4131 ) ) ;
#9415=DIRECTION ( 'NONE',  ( -1.224646799147350002E-16, 0.000000000000000000, 1.000000000000000000 ) ) ;
#9417=LINE ( 'NONE', #7106, #9500 ) ;
#9421=CARTESIAN_POINT ( 'NONE',  ( -16.08946529960249450, -9.036566988620739593, -13.28440143531883244 ) ) ;
#9440=EDGE_CURVE ( 'NONE', #13375, #7843, #13637, .T. ) ;
#9441=CARTESIAN_POINT ( 'NONE',  ( 2.374542637206501272, 7.183219930803497633, 30.65500261342018007 ) ) ;
#9446=CARTESIAN_POINT ( 'NONE',  ( -15.49969986081099904, 64.39262100756199914, 24.21206422150100579 ) ) ;
#9451=COLOUR_RGB ( '', 0.66274510, 0.83137255, 0.94901961) ;
#9452=CARTESIAN_POINT ( 'NONE',  ( 7.499553822109690238, 3.992621007562000557, 24.58036929630707590 ) ) ;
#9458=CARTESIAN_POINT ( 'NONE',  ( -5.499699860810999041, -13.50737899243800122, 6.712064221500998684 ) ) ;
#9462=CARTESIAN_POINT ( 'NONE',  ( -35.84653069491783839, 6.005480809360966177, 29.56784677734614064 ) ) ;
#9464=DIRECTION ( 'NONE',  ( 0.000000000000000000, 2.168404344971008868E-16, -1.000000000000000000 ) ) ;
#9467=EDGE_LOOP ( 'NONE', ( #6050, #12579, #9586, #184 ) ) ;
#9468=FACE_BOUND ( 'NONE', #9041, .T. ) ;
#9473=PRODUCT_DEFINITION ( 'UNKNOWN', '', #12686, #8179 ) ;
#9479=DIRECTION ( 'NONE',  ( 0.000000000000000000, 1.224646799147350002E-16, -1.000000000000000000 ) ) ;
#9485=AXIS2_PLACEMENT_3D ( 'NONE', #3357, #10317, #5350 ) ;
#9486=ORIENTED_EDGE ( 'NONE', *, *, #12311, .F. ) ;
#9488=ORIENTED_EDGE ( 'NONE', *, *, #8789, .F. ) ;
#9493=VERTEX_POINT ( 'NONE', #9897 ) ;
#9499=CARTESIAN_POINT ( 'NONE',  ( -19.99969986081099549, -13.20997340667671160, -13.01695671647154562 ) ) ;
#9500=VECTOR ( 'NONE', #9262, 1000.000000000000000 ) ;
#9503=CARTESIAN_POINT ( 'NONE',  ( -11.59602743870534347, -15.76507124608116150, -13.08455929840592269 ) ) ;
#9513=EDGE_CURVE ( 'NONE', #2844, #10757, #6513, .T. ) ;
#9515=PLANE ( 'NONE',  #1196 ) ;
#9518=DIRECTION ( 'NONE',  ( 0.000000000000000000, -1.000000000000000000, -1.224646799147350002E-16 ) ) ;
#9520=DIRECTION ( 'NONE',  ( 1.000000000000000000, 3.700743415417188632E-16, 0.000000000000000000 ) ) ;
#9521=CARTESIAN_POINT ( 'NONE',  ( -24.89997498294686196, -16.92210204874093549, 60.51485643764996780 ) ) ;
#9525=CARTESIAN_POINT ( 'NONE',  ( 21.91156137581363694, -28.99392143964606205, 26.79309724432473416 ) ) ;
#9536=DIRECTION ( 'NONE',  ( -1.000000000000000000, 0.000000000000000000, 0.000000000000000000 ) ) ;
#9537=CIRCLE ( 'NONE', #6593, 4.499999999999999112 ) ;
#9540=DIRECTION ( 'NONE',  ( 1.000000000000000000, -1.499759782661860071E-32, 1.224646799147350002E-16 ) ) ;
#9542=DIRECTION ( 'NONE',  ( 0.000000000000000000, -1.000000000000000000, -1.224646799147350002E-16 ) ) ;
#9545=CARTESIAN_POINT ( 'NONE',  ( -10.99969986081099904, -13.50737899243800122, -13.01695671647155983 ) ) ;
#9558=ADVANCED_FACE ( 'NONE', ( #9965 ), #14640, .T. ) ;
#9559=DIRECTION ( 'NONE',  ( 0.000000000000000000, -1.000000000000000000, -1.224646799147350002E-16 ) ) ;
#9561=CARTESIAN_POINT ( 'NONE',  ( 7.500245791298697284, 3.992621007561997892, 24.16206422150099442 ) ) ;
#9571=DIRECTION ( 'NONE',  ( 0.000000000000000000, 1.000000000000000000, 1.224646799147350002E-16 ) ) ;
#9575=EDGE_CURVE ( 'NONE', #8805, #947, #8668, .T. ) ;
#9580=( LENGTH_UNIT ( ) NAMED_UNIT ( * ) SI_UNIT ( .MILLI., .METRE. ) );
#9586=ORIENTED_EDGE ( 'NONE', *, *, #849, .T. ) ;
#9587=CARTESIAN_POINT ( 'NONE',  ( 13.85920135429429934, -27.00737899243800300, 43.21206422150100224 ) ) ;
#9595=CARTESIAN_POINT ( 'NONE',  ( -32.76014075162859740, 10.68321993080349763, 16.26994987741149856 ) ) ;
#9599=CARTESIAN_POINT ( 'NONE',  ( -24.10635587892941345, -18.62637863235598346, 60.71193242789581745 ) ) ;
#9602=CARTESIAN_POINT ( 'NONE',  ( 21.92052230653590428, -29.15398386062915037, 21.76268361306444632 ) ) ;
#9614=ORIENTED_EDGE ( 'NONE', *, *, #6545, .T. ) ;
#9620=CARTESIAN_POINT ( 'NONE',  ( -15.49969986081099904, 4.873818854045000037, 24.21206422150099868 ) ) ;
#9638=VECTOR ( 'NONE', #12233, 1000.000000000000000 ) ;
#9639=DIRECTION ( 'NONE',  ( 0.000000000000000000, 1.000000000000000000, 1.224646799147350002E-16 ) ) ;
#9640=EDGE_CURVE ( 'NONE', #259, #9493, #11992, .T. ) ;
#9644=DIRECTION ( 'NONE',  ( 0.000000000000000000, 1.000000000000000000, 0.000000000000000000 ) ) ;
#9645=ORIENTED_EDGE ( 'NONE', *, *, #2353, .F. ) ;
#9649=VERTEX_POINT ( 'NONE', #3082 ) ;
#9651=B_SPLINE_CURVE_WITH_KNOTS ( 'NONE', 3,
 ( #11094, #6342, #14542, #13254, #5205, #540, #5062, #13400, #12169, #1760, #2765, #7419 ),
 .UNSPECIFIED., .F., .F.,
 ( 4, 2, 2, 2, 2, 4 ),
 ( 0.000000000000000000, 0.2500000000000018319, 0.3750000000000028866, 0.4375000000000027756, 0.5000000000000026645, 1.000000000000000000 ),
 .UNSPECIFIED. ) ;
#9653=CARTESIAN_POINT ( 'NONE',  ( -17.49501007863569768, -9.463173585252677711, -13.23580647107073638 ) ) ;
#9667=EDGE_CURVE ( 'NONE', #6551, #12278, #10162, .T. ) ;
#9668=PLANE ( 'NONE',  #7325 ) ;
#9673=CARTESIAN_POINT ( 'NONE',  ( -37.91969009334108165, 5.009117329194947565, 20.24816411459976706 ) ) ;
#9680=CARTESIAN_POINT ( 'NONE',  ( -37.04494295528539993, 12.99262100756199878, 32.26206422150099939 ) ) ;
#9682=DIRECTION ( 'NONE',  ( 1.000000000000000000, 0.000000000000000000, 0.000000000000000000 ) ) ;
#9685=CARTESIAN_POINT ( 'NONE',  ( 7.200737182676100190, 4.873818854045000037, 27.91208557747711083 ) ) ;
#9691=AXIS2_PLACEMENT_3D ( 'NONE', #5280, #12323, #9940 ) ;
#9694=DIRECTION ( 'NONE',  ( 0.000000000000000000, 1.000000000000000000, 1.224646799147350002E-16 ) ) ;
#9696=ORIENTED_EDGE ( 'NONE', *, *, #13256, .F. ) ;
#9701=EDGE_CURVE ( 'NONE', #12465, #13214, #4360, .T. ) ;
#9707=DIRECTION ( 'NONE',  ( -1.000000000000000000, 0.000000000000000000, 0.000000000000000000 ) ) ;
#9711=CARTESIAN_POINT ( 'NONE',  ( -38.20013690429809827, 4.873818854045000037, 20.51204286552489009 ) ) ;
#9712=ORIENTED_EDGE ( 'NONE', *, *, #11118, .F. ) ;
#9714=ORIENTED_EDGE ( 'NONE', *, *, #8945, .F. ) ;
#9732=DIRECTION ( 'NONE',  ( 0.000000000000000000, -1.131341397376178819E-16, 1.000000000000000000 ) ) ;
#9735=ORIENTED_EDGE ( 'NONE', *, *, #14769, .F. ) ;
#9736=DIRECTION ( 'NONE',  ( 0.000000000000000000, 1.272130549049658454E-16, -1.000000000000000000 ) ) ;
#9750=ORIENTED_EDGE ( 'NONE', *, *, #4800, .T. ) ;
#9756=CARTESIAN_POINT ( 'NONE',  ( 21.86810610412018718, -27.84960833679321368, 21.06582514182977306 ) ) ;
#9760=AXIS2_PLACEMENT_3D ( 'NONE', #9158, #11612, #11462 ) ;
#9762=CARTESIAN_POINT ( 'NONE',  ( -15.49969986081099904, 70.81438635534659909, 24.21206422150100579 ) ) ;
#9765=CARTESIAN_POINT ( 'NONE',  ( -15.49969986081099904, 64.39262100756199914, 24.21206422150100579 ) ) ;
#9769=CARTESIAN_POINT ( 'NONE',  ( -31.79969986081099975, 11.99262100756199878, 24.16206422150099797 ) ) ;
#9774=CARTESIAN_POINT ( 'NONE',  ( 4.500300139189000959, -19.50737899243801010, 55.93350807262470425 ) ) ;
#9779=B_SPLINE_CURVE_WITH_KNOTS ( 'NONE', 3,
 ( #5638, #8002, #13909, #12773, #4502, #6853, #2434, #2285, #9462, #3502, #14136, #3658, #3577, #6996, #12617, #6925, #2128, #986, #1126 ),
 .UNSPECIFIED., .F., .F.,
 ( 4, 2, 2, 2, 1, 1, 1, 1, 1, 2, 2, 4 ),
 ( 0.000000000000000000, 0.2500000000003188005, 0.3750000000004767853, 0.4375000000005559442, 0.4687500000005985212, 0.4843750000006151191, 0.4921875000006234457, 0.4960937500006278311, 0.4980468750006310508, 0.4990234375006316614, 0.5000000000006321610, 1.000000000000000000 ),
 .UNSPECIFIED. ) ;
#9782=AXIS2_PLACEMENT_3D ( 'NONE', #6212, #1858, #14412 ) ;
#9783=CARTESIAN_POINT ( 'NONE',  ( 15.21195308717482497, -29.07207680555242035, 2.693057569154425845 ) ) ;
#9792=FACE_OUTER_BOUND ( 'NONE', #9311, .T. ) ;
#9795=DIRECTION ( 'NONE',  ( 0.000000000000000000, 0.000000000000000000, 1.000000000000000000 ) ) ;
#9809=EDGE_CURVE ( 'NONE', #5736, #9278, #1695, .T. ) ;
#9814=EDGE_CURVE ( 'NONE', #8623, #6681, #2992, .T. ) ;
#9817=AXIS2_PLACEMENT_3D ( 'NONE', #345, #8730, #4150 ) ;
#9818=EDGE_CURVE ( 'NONE', #12839, #2212, #1518, .T. ) ;
#9823=EDGE_CURVE ( 'NONE', #7809, #1380, #6201, .T. ) ;
#9827=DIRECTION ( 'NONE',  ( -1.000000000000000000, 0.000000000000000000, 0.000000000000000000 ) ) ;
#9837=CARTESIAN_POINT ( 'NONE',  ( 6.638443592182626141, 5.145091203767020005, 19.98296810155703085 ) ) ;
#9848=CARTESIAN_POINT ( 'NONE',  ( 21.86810272172535363, -26.16575740022191709, 27.35833972362090094 ) ) ;
#9855=EDGE_CURVE ( 'NONE', #9045, #6888, #4144, .T. ) ;
#9860=CARTESIAN_POINT ( 'NONE',  ( 0.8003001391889992266, 20.99262100756200056, 32.26206422150099939 ) ) ;
#9864=ORIENTED_EDGE ( 'NONE', *, *, #4683, .T. ) ;
#9874=AXIS2_PLACEMENT_3D ( 'NONE', #510, #12212, #6377 ) ;
#9877=LINE ( 'NONE', #6271, #14376 ) ;
#9891=CARTESIAN_POINT ( 'NONE',  ( 9.000300139189000959, -27.00737899243800300, 7.712064221501001349 ) ) ;
#9895=CARTESIAN_POINT ( 'NONE',  ( -35.79506410546698447, 6.030134292668329898, 18.82790939717704504 ) ) ;
#9897=CARTESIAN_POINT ( 'NONE',  ( -15.49969986081099904, 2.992621007561999669, 1.212064221501000461 ) ) ;
#9902=CARTESIAN_POINT ( 'NONE',  ( 22.00030013918900096, -27.00737899243800300, 26.71206422150099868 ) ) ;
#9904=DIRECTION ( 'NONE',  ( -1.000000000000000000, 0.000000000000000000, 0.000000000000000000 ) ) ;
#9906=LINE ( 'NONE', #8398, #1590 ) ;
#9909=DIRECTION ( 'NONE',  ( 0.000000000000000000, 1.850371707708594316E-16, -1.000000000000000000 ) ) ;
#9916=EDGE_CURVE ( 'NONE', #14313, #259, #7836, .T. ) ;
#9924=DIRECTION ( 'NONE',  ( 0.000000000000000000, 0.000000000000000000, 1.000000000000000000 ) ) ;
#9925=CARTESIAN_POINT ( 'NONE',  ( 0.1306401100565676154, -27.07585217469822680, -9.967496158821944618 ) ) ;
#9931=ORIENTED_EDGE ( 'NONE', *, *, #14886, .F. ) ;
#9940=DIRECTION ( 'NONE',  ( 1.508455196501571429E-16, 1.131341397376178572E-16, -1.000000000000000000 ) ) ;
#9941=LINE ( 'NONE', #13403, #13162 ) ;
#9942=CARTESIAN_POINT ( 'NONE',  ( -15.49969986081099904, 9.919219809770899232, 24.21206422150099868 ) ) ;
#9946=ORIENTED_EDGE ( 'NONE', *, *, #4571, .F. ) ;
#9947=DIRECTION ( 'NONE',  ( 0.000000000000000000, 0.000000000000000000, 1.000000000000000000 ) ) ;
#9954=DIRECTION ( 'NONE',  ( -1.000000000000000000, 0.000000000000000000, 0.000000000000000000 ) ) ;
#9965=FACE_OUTER_BOUND ( 'NONE', #9038, .T. ) ;
#9969=EDGE_CURVE ( 'NONE', #12278, #6551, #3247, .T. ) ;
#9971=FACE_BOUND ( 'NONE', #8659, .T. ) ;
#9973=DIRECTION ( 'NONE',  ( 0.000000000000000000, 1.000000000000000000, 1.224646799147350002E-16 ) ) ;
#9976=CARTESIAN_POINT ( 'NONE',  ( 4.312229196889595606, 6.261951257096727730, 18.58236366442973519 ) ) ;
#9978=CARTESIAN_POINT ( 'NONE',  ( 14.77511232944436692, -26.09918393201953535, 2.083139152813529904 ) ) ;
#9985=EDGE_LOOP ( 'NONE', ( #13631, #2158, #357, #3248 ) ) ;
#9990=ORIENTED_EDGE ( 'NONE', *, *, #476, .F. ) ;
#9998=DIRECTION ( 'NONE',  ( 0.000000000000000000, 1.000000000000000000, 1.224646799147350002E-16 ) ) ;
#10015=EDGE_CURVE ( 'NONE', #5621, #10814, #1429, .T. ) ;
#10018=DIRECTION ( 'NONE',  ( 0.000000000000000000, 1.000000000000000000, 1.224646799147350002E-16 ) ) ;
#10019=CARTESIAN_POINT ( 'NONE',  ( 15.03585683394451955, -28.72361223820153242, 45.98022787283635893 ) ) ;
#10026=CARTESIAN_POINT ( 'NONE',  ( 1.899771560857192121, 9.436645346035778203, 16.57911348776239180 ) ) ;
#10028=CARTESIAN_POINT ( 'NONE',  ( -14.90935270056153783, -9.036630781709011018, -13.28439369589753483 ) ) ;
#10029=DIRECTION ( 'NONE',  ( 0.000000000000000000, 9.251858538542971581E-17, -1.000000000000000000 ) ) ;
#10031=B_SPLINE_CURVE_WITH_KNOTS ( 'NONE', 3,
 ( #691, #12101, #404, #3987, #5065, #14395, #8568, #13257, #10950, #8647, #13333, #8869, #12555, #5574, #14770, #14991, #3212, #7941, #12397, #12629, #13844, #2070, #3364, #11322, #5504, #4438 ),
 .UNSPECIFIED., .F., .F.,
 ( 4, 2, 2, 1, 2, 2, 2, 2, 1, 2, 2, 2, 2, 4 ),
 ( 0.5000307302539015453, 0.5443642001973365563, 0.5665309351690539508, 0.5886976701407714563, 0.6108644051124889618, 0.6330311400842063563, 0.6773646100276413673, 0.6995313449993587618, 0.7216980799710761563, 0.7438648149427934397, 0.7660315499145107232, 0.8103650198579455122, 0.8325317548296629067, 0.8546984898013801901 ),
 .UNSPECIFIED. ) ;
#10036=CARTESIAN_POINT ( 'NONE',  ( -15.49969986081099904, -32.00737899243799944, 24.21206422150099868 ) ) ;
#10044=CARTESIAN_POINT ( 'NONE',  ( 5.874921005947147279, 5.512834891045747199, 19.41550980370611157 ) ) ;
#10046=CARTESIAN_POINT ( 'NONE',  ( 4.806612929222199071, 12.32432269366989530, 32.26206422150099939 ) ) ;
#10052=CARTESIAN_POINT ( 'NONE',  ( 5.815147591963106599, 5.541088692445907071, 28.99552279544280964 ) ) ;
#10055=CARTESIAN_POINT ( 'NONE',  ( -31.79969986081099975, 11.99262100756199878, 16.16206422150100153 ) ) ;
#10057=CARTESIAN_POINT ( 'NONE',  ( 1.809265100128740311, 10.04760564993946126, 32.04872215841241001 ) ) ;
#10070=AXIS2_PLACEMENT_3D ( 'NONE', #8502, #5069, #9732 ) ;
#10090=EDGE_CURVE ( 'NONE', #12240, #12386, #5809, .T. ) ;
#10092=CARTESIAN_POINT ( 'NONE',  ( -38.20013690429809827, 4.873818854045000037, 20.51204286552489009 ) ) ;
#10098=ORIENTED_EDGE ( 'NONE', *, *, #2334, .T. ) ;
#10100=CARTESIAN_POINT ( 'NONE',  ( 1.817575469379459907, 10.05207975124035613, 16.39402607183602711 ) ) ;
#10101=ORIENTED_EDGE ( 'NONE', *, *, #4108, .T. ) ;
#10103=CARTESIAN_POINT ( 'NONE',  ( -15.49969986081099904, 4.873818854045000037, 24.21206422150099868 ) ) ;
#10105=CARTESIAN_POINT ( 'NONE',  ( 21.85920135429435263, -27.00737899243800300, 27.46206422150099868 ) ) ;
#10109=AXIS2_PLACEMENT_3D ( 'NONE', #5989, #271, #8517 ) ;
#10114=DIRECTION ( 'NONE',  ( 0.000000000000000000, 9.130123557772668334E-17, -1.000000000000000000 ) ) ;
#10116=ORIENTED_EDGE ( 'NONE', *, *, #9809, .T. ) ;
#10118=CARTESIAN_POINT ( 'NONE',  ( -15.49969986081099904, -32.00737899243799944, 24.21206422150100224 ) ) ;
#10125=CARTESIAN_POINT ( 'NONE',  ( 18.53245405280427960, -27.00737899243800300, 39.96206422150099513 ) ) ;
#10129=CARTESIAN_POINT ( 'NONE',  ( -35.80601265084589357, 12.32432269367079591, 32.26206422150099939 ) ) ;
#10139=CARTESIAN_POINT ( 'NONE',  ( 13.85920135429429934, -27.00737899243800300, 21.71206422150100224 ) ) ;
#10141=FACE_OUTER_BOUND ( 'NONE', #445, .T. ) ;
#10150=ORIENTED_EDGE ( 'NONE', *, *, #14663, .F. ) ;
#10153=VERTEX_POINT ( 'NONE', #2679 ) ;
#10161=LINE ( 'NONE', #1919, #8464 ) ;
#10162=B_SPLINE_CURVE_WITH_KNOTS ( 'NONE', 3,
 ( #7889, #4464, #13718, #11269, #2170, #12424, #14866, #1940, #1091, #7808, #948, #12657, #4390, #14790, #12495, #2016, #4539, #6665, #11572, #13797, #11348, #5526, #9042, #12580, #3315, #7962, #6816, #13870, #11495, #10346 ),
 .UNSPECIFIED., .F., .F.,
 ( 4, 2, 2, 2, 2, 2, 2, 2, 2, 2, 2, 2, 2, 2, 4 ),
 ( 0.01102539692970626664, 0.01171599123889527534, 0.01240658554808428231, 0.01309717985727329101, 0.01378777416646229798, 0.01447836847565130668, 0.01516896278484031538, 0.01655015140321834666, 0.01793134002159637447, 0.01862193433078539531, 0.01931252863997440922, 0.02000312294916342659, 0.02069371725835244050, 0.02138431156754145440, 0.02207490587673047178 ),
 .UNSPECIFIED. ) ;
#10171=CARTESIAN_POINT ( 'NONE',  ( -15.49968909271368211, -3.507379016232285096, 61.71092834827113194 ) ) ;
#10184=EDGE_CURVE ( 'NONE', #1107, #3863, #1782, .T. ) ;
#10202=AXIS2_PLACEMENT_3D ( 'NONE', #6077, #10764, #12066 ) ;
#10205=CARTESIAN_POINT ( 'NONE',  ( 15.84215789323456569, -24.14741025098728144, 3.617636113674804310 ) ) ;
#10209=DIRECTION ( 'NONE',  ( 0.000000000000000000, 1.000000000000000000, 1.224646799147350002E-16 ) ) ;
#10220=VERTEX_POINT ( 'NONE', #13818 ) ;
#10232=CARTESIAN_POINT ( 'NONE',  ( 2.377116011596400291, -23.18484177525213141, -8.848022433876742809 ) ) ;
#10236=CARTESIAN_POINT ( 'NONE',  ( -15.49969986081100082, 22.99262100756200411, 8.337064221501000461 ) ) ;
#10241=CARTESIAN_POINT ( 'NONE',  ( -15.49969986081099904, 20.99262100756200056, 16.16206422150100153 ) ) ;
#10243=AXIS2_PLACEMENT_3D ( 'NONE', #10907, #6226, #13219 ) ;
#10248=DIRECTION ( 'NONE',  ( 0.000000000000000000, 0.000000000000000000, 1.000000000000000000 ) ) ;
#10250=AXIS2_PLACEMENT_3D ( 'NONE', #9762, #1723, #4248 ) ;
#10255=CARTESIAN_POINT ( 'NONE',  ( -25.48037379874287467, -12.85419436533228144, 60.35950308624435934 ) ) ;
#10262=LINE ( 'NONE', #3382, #2680 ) ;
#10289=CARTESIAN_POINT ( 'NONE',  ( -16.95106854142316877, -17.77697586203957059, -13.26081966632196263 ) ) ;
#10305=ADVANCED_FACE ( 'NONE', ( #8062 ), #50, .T. ) ;
#10311=CONICAL_SURFACE ( 'NONE', #3721, 15.87500000000000355, 0.1448623279155291654 ) ;
#10317=DIRECTION ( 'NONE',  ( 0.000000000000000000, 1.224646799147350002E-16, -1.000000000000000000 ) ) ;
#10318=ADVANCED_FACE ( 'NONE', ( #12676 ), #9066, .F. ) ;
#10322=AXIS2_PLACEMENT_3D ( 'NONE', #180, #14174, #12963 ) ;
#10324=LINE ( 'NONE', #5801, #6484 ) ;
#10328=CARTESIAN_POINT ( 'NONE',  ( 18.47600606207883445, -27.91756206037096888, 40.08355722636073182 ) ) ;
#10330=CARTESIAN_POINT ( 'NONE',  ( -23.43779763612971223, -7.414416043088839281, 60.86287324052170078 ) ) ;
#10335=ORIENTED_EDGE ( 'NONE', *, *, #388, .T. ) ;
#10336=DIRECTION ( 'NONE',  ( 0.000000000000000000, -1.000000000000000000, -1.224646799147350002E-16 ) ) ;
#10341=AXIS2_PLACEMENT_3D ( 'NONE', #2657, #14362, #8461 ) ;
#10342=AXIS2_PLACEMENT_3D ( 'NONE', #9373, #13739, #4482 ) ;
#10346=CARTESIAN_POINT ( 'NONE',  ( 14.68618260102869932, -27.00737899243800300, 46.46206422150099513 ) ) ;
#10352=CYLINDRICAL_SURFACE ( 'NONE', #5662, 22.99999999999999645 ) ;
#10362=DIRECTION ( 'NONE',  ( -1.000000000000000000, 0.000000000000000000, 0.000000000000000000 ) ) ;
#10365=CARTESIAN_POINT ( 'NONE',  ( -15.49969986081099904, 13.89262100756199736, 29.46206422150100224 ) ) ;
#10367=ORIENTED_EDGE ( 'NONE', *, *, #9969, .T. ) ;
#10372=ORIENTED_EDGE ( 'NONE', *, *, #5868, .F. ) ;
#10377=EDGE_CURVE ( 'NONE', #7809, #4749, #5591, .T. ) ;
#10380=DIRECTION ( 'NONE',  ( -1.000000000000000000, 1.499759782661860071E-32, -1.224646799147350002E-16 ) ) ;
#10382=FACE_OUTER_BOUND ( 'NONE', #4353, .T. ) ;
#10390=CARTESIAN_POINT ( 'NONE',  ( -15.49969986081099904, 71.39262100756199914, 24.21206422150100579 ) ) ;
#10394=EDGE_CURVE ( 'NONE', #13305, #1644, #12202, .T. ) ;
#10400=CARTESIAN_POINT ( 'NONE',  ( 9.000300139189000959, -19.50737899243800300, 52.60220335465780295 ) ) ;
#10410=CARTESIAN_POINT ( 'NONE',  ( -15.49969986081099549, 2.992621007561993451, 52.21206422150100224 ) ) ;
#10418=ADVANCED_FACE ( 'NONE', ( #13948 ), #2984, .F. ) ;
#10419=FACE_BOUND ( 'NONE', #13058, .T. ) ;
#10420=EDGE_LOOP ( 'NONE', ( #7505, #2866, #12353, #5242, #2904, #465, #8105, #6209 ) ) ;
#10435=EDGE_CURVE ( 'NONE', #4771, #10220, #14029, .T. ) ;
#10440=AXIS2_PLACEMENT_3D ( 'NONE', #8635, #7627, #1745 ) ;
#10443=ORIENTED_EDGE ( 'NONE', *, *, #4575, .T. ) ;
#10454=VECTOR ( 'NONE', #3937, 1000.000000000000000 ) ;
#10461=ORIENTED_EDGE ( 'NONE', *, *, #13256, .T. ) ;
#10467=CARTESIAN_POINT ( 'NONE',  ( -38.20013690429809827, 4.873818854045000037, 27.91208557747711083 ) ) ;
#10468=ORIENTED_EDGE ( 'NONE', *, *, #6382, .T. ) ;
#10476=CYLINDRICAL_SURFACE ( 'NONE', #6493, 37.50000000000000000 ) ;
#10486=CIRCLE ( 'NONE', #9760, 2.500000000000000444 ) ;
#10489=ORIENTED_EDGE ( 'NONE', *, *, #14148, .T. ) ;
#10491=FACE_OUTER_BOUND ( 'NONE', #12735, .T. ) ;
#10495=DIRECTION ( 'NONE',  ( 0.000000000000000000, -1.000000000000000000, -1.224646799147350002E-16 ) ) ;
#10501=EDGE_CURVE ( 'NONE', #13375, #8329, #10944, .T. ) ;
#10516=CARTESIAN_POINT ( 'NONE',  ( -2.216578225681298697, -31.14135358865360104, 59.46602571891969546 ) ) ;
#10526=EDGE_LOOP ( 'NONE', ( #5958, #1851, #1941, #2756 ) ) ;
#10530=CARTESIAN_POINT ( 'NONE',  ( -31.79969986081099975, 3.992621007561997892, 24.26206422150100650 ) ) ;
#10532=ORIENTED_EDGE ( 'NONE', *, *, #1737, .T. ) ;
#10535=VERTEX_POINT ( 'NONE', #6241 ) ;
#10538=CARTESIAN_POINT ( 'NONE',  ( 13.85920135429429934, -27.00737899243800300, 24.21206422150099868 ) ) ;
#10540=AXIS2_PLACEMENT_3D ( 'NONE', #12119, #13643, #4078 ) ;
#10548=CIRCLE ( 'NONE', #5175, 23.00000000000000000 ) ;
#10549=VECTOR ( 'NONE', #1547, 1000.000000000000000 ) ;
#10554=ORIENTED_EDGE ( 'NONE', *, *, #6887, .F. ) ;
#10562=CARTESIAN_POINT ( 'NONE',  ( -37.04494295528539993, 20.99262100756200056, 32.26206422150099939 ) ) ;
#10571=CARTESIAN_POINT ( 'NONE',  ( 18.10089137489735123, -24.75016685675518247, 7.560273441128909866 ) ) ;
#10573=AXIS2_PLACEMENT_3D ( 'NONE', #8280, #11653, #14183 ) ;
#10575=CARTESIAN_POINT ( 'NONE',  ( -15.49969986081099904, 70.89785811302749607, 15.32568252027467004 ) ) ;
#10579=ORIENTED_EDGE ( 'NONE', *, *, #7090, .F. ) ;
#10583=FACE_OUTER_BOUND ( 'NONE', #3028, .T. ) ;
#10591=CARTESIAN_POINT ( 'NONE',  ( -10.99969986081100082, -13.50737899243800122, 6.712064221500998684 ) ) ;
#10594=ORIENTED_EDGE ( 'NONE', *, *, #9157, .T. ) ;
#10598=ORIENTED_EDGE ( 'NONE', *, *, #6368, .F. ) ;
#10599=CARTESIAN_POINT ( 'NONE',  ( 21.99138435360703525, -30.15310640139978915, 23.36840399548836444 ) ) ;
#10605=EDGE_LOOP ( 'NONE', ( #11774, #8748, #7390, #2457, #12644 ) ) ;
#10607=AXIS2_PLACEMENT_3D ( 'NONE', #5024, #2928, #9682 ) ;
#10611=ORIENTED_EDGE ( 'NONE', *, *, #2164, .F. ) ;
#10612=CARTESIAN_POINT ( 'NONE',  ( -15.49969986081099904, -13.50737899243800122, 6.712064221500998684 ) ) ;
#10614=CONICAL_SURFACE ( 'NONE', #5967, 15.87500000000000355, 0.1448623279155291654 ) ;
#10618=ORIENTED_EDGE ( 'NONE', *, *, #6247, .T. ) ;
#10621=CARTESIAN_POINT ( 'NONE',  ( -15.49969986081099904, 20.99262100756200056, 24.21206422150100224 ) ) ;
#10622=DIRECTION ( 'NONE',  ( 0.000000000000000000, 0.000000000000000000, 1.000000000000000000 ) ) ;
#10626=CARTESIAN_POINT ( 'NONE',  ( -23.49969986081099904, -19.50737899243800300, 6.712064221500998684 ) ) ;
#10633=EDGE_CURVE ( 'NONE', #6219, #5382, #6879, .T. ) ;
#10641=CARTESIAN_POINT ( 'NONE',  ( -31.79969986081099975, 20.99262100756200056, 24.21206422150100224 ) ) ;
#10643=CARTESIAN_POINT ( 'NONE',  ( -5.499699860810999041, -19.50737899243799589, -123.9247733198440073 ) ) ;
#10645=CARTESIAN_POINT ( 'NONE',  ( 18.53245405280430802, -27.00737899243800300, 8.462064221501000461 ) ) ;
#10652=ORIENTED_EDGE ( 'NONE', *, *, #14224, .T. ) ;
#10654=ORIENTED_EDGE ( 'NONE', *, *, #8124, .T. ) ;
#10655=EDGE_LOOP ( 'NONE', ( #511, #1241, #4582, #1730, #8388 ) ) ;
#10658=ORIENTED_EDGE ( 'NONE', *, *, #6951, .F. ) ;
#10661=B_SPLINE_CURVE_WITH_KNOTS ( 'NONE', 3,
 ( #13510, #10046, #7530, #14577 ),
 .UNSPECIFIED., .F., .F.,
 ( 4, 4 ),
 ( 0.01169941957287599921, 0.01381006638855979997 ),
 .UNSPECIFIED. ) ;
#10669=EDGE_CURVE ( 'NONE', #13407, #4277, #13748, .T. ) ;
#10671=ORIENTED_EDGE ( 'NONE', *, *, #1369, .F. ) ;
#10672=ORIENTED_EDGE ( 'NONE', *, *, #3385, .F. ) ;
#10684=CARTESIAN_POINT ( 'NONE',  ( 22.00030013918900096, -27.00737899243800300, 40.71206422150099513 ) ) ;
#10688=CARTESIAN_POINT ( 'NONE',  ( 9.000300139189000959, -27.00737899243800300, 24.21206422150099868 ) ) ;
#10703=CARTESIAN_POINT ( 'NONE',  ( -6.891327302372677543, -18.62408673770649159, 60.71152943577731520 ) ) ;
#10705=VERTEX_POINT ( 'NONE', #11297 ) ;
#10712=CARTESIAN_POINT ( 'NONE',  ( 7.361522891262090695, 4.383170266556664529, 21.67185847294893719 ) ) ;
#10721=CARTESIAN_POINT ( 'NONE',  ( -34.24293707257970709, 11.48902252484896991, 16.16206422150067823 ) ) ;
#10729=LINE ( 'NONE', #106, #5438 ) ;
#10732=ORIENTED_EDGE ( 'NONE', *, *, #1951, .F. ) ;
#10733=ORIENTED_EDGE ( 'NONE', *, *, #9814, .F. ) ;
#10737=CARTESIAN_POINT ( 'NONE',  ( -15.49969986081099904, 64.39262100756199914, 18.96206422150100579 ) ) ;
#10738=VECTOR ( 'NONE', #6655, 1000.000000000000000 ) ;
#10744=DIRECTION ( 'NONE',  ( 0.000000000000000000, 1.224646799147350002E-16, -1.000000000000000000 ) ) ;
#10754=CARTESIAN_POINT ( 'NONE',  ( 21.98610757316710718, -30.09037826958212491, 23.16186116307340725 ) ) ;
#10757=VERTEX_POINT ( 'NONE', #11226 ) ;
#10764=DIRECTION ( 'NONE',  ( -1.000000000000000000, 0.000000000000000000, 0.000000000000000000 ) ) ;
#10768=VERTEX_POINT ( 'NONE', #10139 ) ;
#10771=DIRECTION ( 'NONE',  ( 1.000000000000000000, -3.922012711866029438E-32, 3.202566417187950042E-16 ) ) ;
#10772=ORIENTED_EDGE ( 'NONE', *, *, #9701, .T. ) ;
#10773=DIRECTION ( 'NONE',  ( 0.000000000000000000, 0.000000000000000000, 1.000000000000000000 ) ) ;
#10774=FACE_OUTER_BOUND ( 'NONE', #5673, .T. ) ;
#10776=CARTESIAN_POINT ( 'NONE',  ( -37.04494295528539993, 12.99262100756199878, 16.16206422150100153 ) ) ;
#10782=CARTESIAN_POINT ( 'NONE',  ( 15.62491684846984619, -29.63902260056506321, 3.294372889119066450 ) ) ;
#10789=ORIENTED_EDGE ( 'NONE', *, *, #14575, .T. ) ;
#10797=DIRECTION ( 'NONE',  ( -1.000000000000000000, 0.000000000000000000, 0.000000000000000000 ) ) ;
#10802=CARTESIAN_POINT ( 'NONE',  ( 17.94083381668699673, -24.45944232969977250, 7.241130984151665118 ) ) ;
#10808=FILL_AREA_STYLE ('',( #6121 ) ) ;
#10811=ADVANCED_FACE ( 'NONE', ( #11522 ), #8582, .T. ) ;
#10814=VERTEX_POINT ( 'NONE', #5706 ) ;
#10827=ORIENTED_EDGE ( 'NONE', *, *, #8823, .T. ) ;
#10829=EDGE_CURVE ( 'NONE', #4184, #8556, #41, .T. ) ;
#10842=EDGE_LOOP ( 'NONE', ( #12658, #7057, #11573, #14754 ) ) ;
#10861=CARTESIAN_POINT ( 'NONE',  ( 16.55868115085372594, -30.23116488229778653, 4.755404724957913665 ) ) ;
#10876=DIRECTION ( 'NONE',  ( 0.000000000000000000, -1.508455196501571676E-16, 1.000000000000000000 ) ) ;
#10885=CARTESIAN_POINT ( 'NONE',  ( -15.49969986081099904, -2.007378992438000331, 24.21206422150100579 ) ) ;
#10892=DIRECTION ( 'NONE',  ( 0.000000000000000000, -2.185478394931410082E-16, 1.000000000000000000 ) ) ;
#10898=CARTESIAN_POINT ( 'NONE',  ( -37.01777924068312586, 5.443421374451959949, 19.56527334556399111 ) ) ;
#10901=CARTESIAN_POINT ( 'NONE',  ( -24.80291049273179027, -17.17778628407305774, 60.53990586317451061 ) ) ;
#10902=ORIENTED_EDGE ( 'NONE', *, *, #562, .F. ) ;
#10903=ORIENTED_EDGE ( 'NONE', *, *, #3749, .T. ) ;
#10905=ORIENTED_EDGE ( 'NONE', *, *, #1799, .T. ) ;
#10907=CARTESIAN_POINT ( 'NONE',  ( -15.49969986081099904, 2.992621007561997004, 24.21206422150099868 ) ) ;
#10923=PRODUCT ( 'Tapered Toolholder Shank', 'Tapered Toolholder Shank', '', ( #7693 ) ) ;
#10929=CARTESIAN_POINT ( 'NONE',  ( 13.85920135429429934, -27.00737899243800300, 43.21206422150100224 ) ) ;
#10941=ORIENTED_EDGE ( 'NONE', *, *, #5503, .F. ) ;
#10943=ORIENTED_EDGE ( 'NONE', *, *, #558, .F. ) ;
#10944=LINE ( 'NONE', #5200, #12270 ) ;
#10950=CARTESIAN_POINT ( 'NONE',  ( -10.48883820339395179, -4.847810977035234892, 61.37690497805530754 ) ) ;
#10956=CIRCLE ( 'NONE', #12173, 8.314203600725839749 ) ;
#10962=ORIENTED_EDGE ( 'NONE', *, *, #8945, .T. ) ;
#10964=AXIS2_PLACEMENT_3D ( 'NONE', #12973, #14037, #2478 ) ;
#10966=ORIENTED_EDGE ( 'NONE', *, *, #549, .T. ) ;
#10967=CARTESIAN_POINT ( 'NONE',  ( -11.92312357957555236, -10.76045428471250709, -13.11735313252289181 ) ) ;
#10971=CARTESIAN_POINT ( 'NONE',  ( -36.81454731355714216, 5.541088692458852272, 19.42860564753712538 ) ) ;
#10977=ORIENTED_EDGE ( 'NONE', *, *, #2334, .F. ) ;
#10990=CARTESIAN_POINT ( 'NONE',  ( -35.49969986081099904, -19.50737899243800300, -7.509379629622798369 ) ) ;
#10993=CARTESIAN_POINT ( 'NONE',  ( 21.99139727573606606, -23.86149664705925488, 23.36879478108531316 ) ) ;
#10999=CARTESIAN_POINT ( 'NONE',  ( -15.49969986081099549, -2.007378992438005216, 52.21206422150100224 ) ) ;
#11003=DIRECTION ( 'NONE',  ( -1.000000000000000000, 0.000000000000000000, 0.000000000000000000 ) ) ;
#11005=CARTESIAN_POINT ( 'NONE',  ( -32.87720281798463873, 9.589597845032626466, 31.89482592002004679 ) ) ;
#11024=ORIENTED_EDGE ( 'NONE', *, *, #7088, .F. ) ;
#11031=ORIENTED_EDGE ( 'NONE', *, *, #9440, .T. ) ;
#11036=B_SPLINE_CURVE_WITH_KNOTS ( 'NONE', 3,
 ( #3222, #11558, #10255, #5738, #3524, #5658, #4602, #12564, #9026, #11332, #9103, #9330, #3303, #10330, #9255, #14851, #6945, #13855, #13931, #3446, #8098, #12797, #2307, #6649, #5812, #11627, #14006, #10171 ),
 .UNSPECIFIED., .F., .F.,
 ( 4, 2, 2, 2, 2, 2, 1, 2, 2, 2, 2, 1, 2, 2, 4 ),
 ( 0.1453386670947538206, 0.1675069210422008015, 0.1785910480159242086, 0.1896751749896476158, 0.2340116828845410779, 0.2561799368319878090, 0.2783481907794345123, 0.3005164447268813266, 0.3226846986743281409, 0.3670212065692216030, 0.3891894605166682508, 0.4113577144641149541, 0.4335259684115615464, 0.4556942223590082497, 0.5000307302539015453 ),
 .UNSPECIFIED. ) ;
#11046=VERTEX_POINT ( 'NONE', #9595 ) ;
#11047=LINE ( 'NONE', #14567, #4821 ) ;
#11059=CARTESIAN_POINT ( 'NONE',  ( 7.200737182676100190, 4.873818854045000037, 20.51204286552489009 ) ) ;
#11060=PLANE ( 'NONE',  #7563 ) ;
#11061=CARTESIAN_POINT ( 'NONE',  ( -31.79969986081099975, 20.99262100756200056, 16.16206422150100153 ) ) ;
#11080=CARTESIAN_POINT ( 'NONE',  ( -15.49969986081099904, 64.39262100756199914, 30.46206422150100934 ) ) ;
#11082=ORIENTED_EDGE ( 'NONE', *, *, #4560, .T. ) ;
#11092=CARTESIAN_POINT ( 'NONE',  ( 7.000300139189000070, -32.00737899243799944, -5.787935778498998651 ) ) ;
#11094=CARTESIAN_POINT ( 'NONE',  ( -33.37394235882850069, 7.183219930803497633, 17.76912582958182085 ) ) ;
#11110=DIRECTION ( 'NONE',  ( 0.000000000000000000, -1.000000000000000000, -1.224646799147350002E-16 ) ) ;
#11113=CARTESIAN_POINT ( 'NONE',  ( -14.04785070661220736, -9.237812854699480880, -13.26081354841219451 ) ) ;
#11115=DIRECTION ( 'NONE',  ( -1.224646799147350002E-16, -1.224646799147350002E-16, 1.000000000000000000 ) ) ;
#11117=EDGE_CURVE ( 'NONE', #1266, #13484, #14716, .T. ) ;
#11118=EDGE_CURVE ( 'NONE', #11355, #14421, #1991, .T. ) ;
#11119=AXIS2_PLACEMENT_3D ( 'NONE', #10643, #3687, #3531 ) ;
#11121=CARTESIAN_POINT ( 'NONE',  ( -35.91640051037089165, 5.971976172174843001, 18.89405436573536079 ) ) ;
#11123=ORIENTED_EDGE ( 'NONE', *, *, #14663, .T. ) ;
#11126=LINE ( 'NONE', #14493, #908 ) ;
#11129=CARTESIAN_POINT ( 'NONE',  ( 21.85920135429434907, -27.00737899243800300, 20.96206422150100224 ) ) ;
#11140=FACE_BOUND ( 'NONE', #7481, .T. ) ;
#11142=ORIENTED_EDGE ( 'NONE', *, *, #13236, .F. ) ;
#11150=DIRECTION ( 'NONE',  ( 0.000000000000000000, 1.000000000000000000, 1.224646799147350002E-16 ) ) ;
#11157=CARTESIAN_POINT ( 'NONE',  ( -33.10531216574866420, 8.250019247744555528, 31.36164418743403459 ) ) ;
#11172=DIRECTION ( 'NONE',  ( -1.000000000000000000, 0.000000000000000000, 0.000000000000000000 ) ) ;
#11176=CARTESIAN_POINT ( 'NONE',  ( -38.46438895118065915, 4.086072560925112285, 22.89991886225540796 ) ) ;
#11179=ORIENTED_EDGE ( 'NONE', *, *, #9855, .T. ) ;
#11180=CARTESIAN_POINT ( 'NONE',  ( 14.70450431974454020, -27.46836090773456007, 46.43726578852947995 ) ) ;
#11200=DIRECTION ( 'NONE',  ( 0.000000000000000000, -1.000000000000000000, -1.224646799147350002E-16 ) ) ;
#11202=VERTEX_POINT ( 'NONE', #5231 ) ;
#11203=CIRCLE ( 'NONE', #953, 6.250000000000001776 ) ;
#11207=FACE_OUTER_BOUND ( 'NONE', #3954, .T. ) ;
#11224=LINE ( 'NONE', #9068, #3274 ) ;
#11226=CARTESIAN_POINT ( 'NONE',  ( 9.000300139189000959, -32.00737899243799944, -4.178074911655800250 ) ) ;
#11229=CARTESIAN_POINT ( 'NONE',  ( -15.49969986081099904, 64.39262100756199914, 17.96206422150100579 ) ) ;
#11231=CIRCLE ( 'NONE', #12953, 3.249999999999999556 ) ;
#11237=CARTESIAN_POINT ( 'NONE',  ( -33.37394235882850069, 7.183219930803497633, 30.65500261342018007 ) ) ;
#11241=ORIENTED_EDGE ( 'NONE', *, *, #7434, .F. ) ;
#11246=AXIS2_PLACEMENT_3D ( 'NONE', #7437, #3929, #10892 ) ;
#11250=CARTESIAN_POINT ( 'NONE',  ( 9.000300139189000959, -32.00737899243799944, 52.60220335465780295 ) ) ;
#11254=CARTESIAN_POINT ( 'NONE',  ( 15.51282817721622109, -29.51029345576456819, 45.29537398124922021 ) ) ;
#11256=VERTEX_POINT ( 'NONE', #3390 ) ;
#11261=CARTESIAN_POINT ( 'NONE',  ( 1.877803096367266278, 9.589597844970082718, 16.52930252299240621 ) ) ;
#11268=ORIENTED_EDGE ( 'NONE', *, *, #997, .T. ) ;
#11269=CARTESIAN_POINT ( 'NONE',  ( 18.47578936866889876, -26.09629254026139122, 40.08401990837758433 ) ) ;
#11270=ORIENTED_EDGE ( 'NONE', *, *, #8676, .F. ) ;
#11275=FACE_OUTER_BOUND ( 'NONE', #10420, .T. ) ;
#11279=CIRCLE ( 'NONE', #4450, 19.00000000000000000 ) ;
#11282=CARTESIAN_POINT ( 'NONE',  ( 4.806612929223899044, 12.32432269367079591, 16.16206422150100153 ) ) ;
#11289=CYLINDRICAL_SURFACE ( 'NONE', #14141, 10.00000000000000000 ) ;
#11290=VERTEX_POINT ( 'NONE', #11642 ) ;
#11292=ADVANCED_FACE ( 'NONE', ( #6734, #10419, #6814, #1089 ), #8040, .T. ) ;
#11297=CARTESIAN_POINT ( 'NONE',  ( -35.18530787408279537, 11.99262100756689620, 16.16206422150100153 ) ) ;
#11303=CIRCLE ( 'NONE', #10070, 22.99999999999999645 ) ;
#11314=ORIENTED_EDGE ( 'NONE', *, *, #10633, .T. ) ;
#11322=CARTESIAN_POINT ( 'NONE',  ( -5.519619651378201652, -12.85420092285971805, 60.35966704321151610 ) ) ;
#11325=CARTESIAN_POINT ( 'NONE',  ( -35.49969986081099904, -19.50737899243800300, -123.9247733198440073 ) ) ;
#11332=CARTESIAN_POINT ( 'NONE',  ( -24.60545001190342873, -9.363048095758424338, 60.58996776729609479 ) ) ;
#11340=ADVANCED_FACE ( 'NONE', ( #4997 ), #12029, .F. ) ;
#11348=CARTESIAN_POINT ( 'NONE',  ( 15.51479836175852789, -24.50194921392514757, 45.29248735876494436 ) ) ;
#11354=FACE_OUTER_BOUND ( 'NONE', #12634, .T. ) ;
#11355=VERTEX_POINT ( 'NONE', #10575 ) ;
#11357=EDGE_CURVE ( 'NONE', #3429, #9206, #10729, .T. ) ;
#11358=FACE_OUTER_BOUND ( 'NONE', #14060, .T. ) ;
#11361=CARTESIAN_POINT ( 'NONE',  ( 14.95706336429091721, -25.48138479685667690, 2.334038900917459358 ) ) ;
#11364=DIRECTION ( 'NONE',  ( 0.000000000000000000, 1.000000000000000000, 1.224646799147350002E-16 ) ) ;
#11397=CARTESIAN_POINT ( 'NONE',  ( 4.500300139189000959, -19.50737899243801010, -123.9247733198440073 ) ) ;
#11401=CARTESIAN_POINT ( 'NONE',  ( 14.77482671525745594, -27.91392081745070897, 46.34137906563161380 ) ) ;
#11412=ADVANCED_FACE ( 'NONE', ( #8270 ), #1546, .F. ) ;
#11413=AXIS2_PLACEMENT_3D ( 'NONE', #9769, #9540, #5107 ) ;
#11414=DIRECTION ( 'NONE',  ( 0.000000000000000000, -1.224646799147350002E-16, 1.000000000000000000 ) ) ;
#11422=VERTEX_POINT ( 'NONE', #5977 ) ;
#11426=B_SPLINE_CURVE_WITH_KNOTS ( 'NONE', 3,
 ( #3216, #3058, #2785, #11176, #14843, #12117, #7791, #10092 ),
 .UNSPECIFIED., .F., .F.,
 ( 4, 2, 2, 4 ),
 ( 0.000000000000000000, 0.2499999999999999445, 0.4999999999999998890, 1.000000000000000000 ),
 .UNSPECIFIED. ) ;
#11435=FACE_OUTER_BOUND ( 'NONE', #3621, .T. ) ;
#11436=CARTESIAN_POINT ( 'NONE',  ( -15.49969986081099727, 22.99262100756199700, 39.83706422150100224 ) ) ;
#11438=DIRECTION ( 'NONE',  ( 0.000000000000000000, 1.000000000000000000, 1.224646799147350002E-16 ) ) ;
#11439=CARTESIAN_POINT ( 'NONE',  ( -19.99969986081099549, -13.80506132690247512, -13.01695671647155095 ) ) ;
#11441=ORIENTED_EDGE ( 'NONE', *, *, #8537, .F. ) ;
#11451=CARTESIAN_POINT ( 'NONE',  ( -15.49969986081099727, 70.89785811302749607, 33.09844592272734332 ) ) ;
#11455=PLANE ( 'NONE',  #6238 ) ;
#11456=CARTESIAN_POINT ( 'NONE',  ( -2.216578225681298697, -32.00737899243799944, -10.85656391856669778 ) ) ;
#11462=DIRECTION ( 'NONE',  ( 0.000000000000000000, 0.000000000000000000, 1.000000000000000000 ) ) ;
#11471=CARTESIAN_POINT ( 'NONE',  ( 9.000300139189000959, -32.00737899243799944, 52.60220335465780295 ) ) ;
#11478=CARTESIAN_POINT ( 'NONE',  ( 14.68618260102869932, -27.00737899243800300, 46.46206422150099513 ) ) ;
#11484=EDGE_CURVE ( 'NONE', #10814, #12333, #11303, .T. ) ;
#11485=AXIS2_PLACEMENT_3D ( 'NONE', #4004, #11115, #5081 ) ;
#11490=( NAMED_UNIT ( * ) PLANE_ANGLE_UNIT ( ) SI_UNIT ( $, .RADIAN. ) );
#11492=CARTESIAN_POINT ( 'NONE',  ( 9.000300139189000959, -19.50737899243800300, 24.21206422150099868 ) ) ;
#11495=CARTESIAN_POINT ( 'NONE',  ( 14.68618260102869577, -26.77367873612697480, 46.46206422150098803 ) ) ;
#11510=CARTESIAN_POINT ( 'NONE',  ( -15.49969986081099904, 71.39262100756199914, 24.21206422150100579 ) ) ;
#11522=FACE_OUTER_BOUND ( 'NONE', #8948, .T. ) ;
#11540=EDGE_LOOP ( 'NONE', ( #8008, #8683, #10772, #2090, #14865 ) ) ;
#11542=VERTEX_POINT ( 'NONE', #6490 ) ;
#11549=AXIS2_PLACEMENT_3D ( 'NONE', #5361, #10018, #7715 ) ;
#11554=ORIENTED_EDGE ( 'NONE', *, *, #14784, .T. ) ;
#11558=CARTESIAN_POINT ( 'NONE',  ( -25.49738368519668086, -13.18106784639022244, 60.35478574090821269 ) ) ;
#11565=DIRECTION ( 'NONE',  ( 0.000000000000000000, -1.000000000000000000, -1.224646799147350002E-16 ) ) ;
#11568=CIRCLE ( 'NONE', #14018, 2.499999999999998668 ) ;
#11572=CARTESIAN_POINT ( 'NONE',  ( 15.84905121855136478, -24.16036003417319122, 44.79232149582683320 ) ) ;
#11573=ORIENTED_EDGE ( 'NONE', *, *, #12456, .T. ) ;
#11575=ORIENTED_EDGE ( 'NONE', *, *, #6093, .T. ) ;
#11580=EDGE_CURVE ( 'NONE', #3001, #970, #4226, .T. ) ;
#11592=CARTESIAN_POINT ( 'NONE',  ( -15.49969986081099904, 20.99262100756200056, 24.21206422150099868 ) ) ;
#11606=DIRECTION ( 'NONE',  ( -3.202566417187950042E-16, 0.000000000000000000, 1.000000000000000000 ) ) ;
#11607=LINE ( 'NONE', #11456, #8407 ) ;
#11612=DIRECTION ( 'NONE',  ( -1.000000000000000000, 0.000000000000000000, 0.000000000000000000 ) ) ;
#11619=CARTESIAN_POINT ( 'NONE',  ( -7.176549351029851032, -19.07651164606311056, 60.77823124794023357 ) ) ;
#11623=ORIENTED_EDGE ( 'NONE', *, *, #549, .F. ) ;
#11627=CARTESIAN_POINT ( 'NONE',  ( -16.80342572160717651, -3.572236342509832241, 61.69496154213114636 ) ) ;
#11639=CARTESIAN_POINT ( 'NONE',  ( 17.24950932937950299, -23.81275511923810839, 5.938204047008457387 ) ) ;
#11642=CARTESIAN_POINT ( 'NONE',  ( -28.78282149594069850, -32.00737899243799944, 59.28069236156870403 ) ) ;
#11643=EDGE_LOOP ( 'NONE', ( #11142, #9645, #5090, #1261 ) ) ;
#11644=CARTESIAN_POINT ( 'NONE',  ( -15.49969986081099371, -18.00737899243799944, -13.28793577849899776 ) ) ;
#11653=DIRECTION ( 'NONE',  ( 0.000000000000000000, -1.000000000000000000, -1.224646799147350002E-16 ) ) ;
#11678=LINE ( 'NONE', #10530, #158 ) ;
#11683=CARTESIAN_POINT ( 'NONE',  ( -15.49969986081099904, -32.00737899243799944, 24.21206422150099868 ) ) ;
#11693=LINE ( 'NONE', #4664, #4274 ) ;
#11705=VERTEX_POINT ( 'NONE', #6868 ) ;
#11707=ORIENTED_EDGE ( 'NONE', *, *, #5057, .F. ) ;
#11712=CARTESIAN_POINT ( 'NONE',  ( -28.78282149594069850, -31.14135358865360104, -10.85656391856669778 ) ) ;
#11717=EDGE_CURVE ( 'NONE', #8623, #5152, #8862, .T. ) ;
#11718=DIRECTION ( 'NONE',  ( 0.000000000000000000, 1.000000000000000000, 1.224646799147350002E-16 ) ) ;
#11723=EDGE_LOOP ( 'NONE', ( #9160, #4064 ) ) ;
#11726=EDGE_LOOP ( 'NONE', ( #1042, #5694, #14293, #14295 ) ) ;
#11731=B_SPLINE_CURVE_WITH_KNOTS ( 'NONE', 3,
 ( #5635, #13977, #5932, #13828 ),
 .UNSPECIFIED., .F., .F.,
 ( 4, 4 ),
 ( 0.000000000000000000, 1.000000000000000000 ),
 .UNSPECIFIED. ) ;
#11732=DIRECTION ( 'NONE',  ( 0.000000000000000000, 0.000000000000000000, 1.000000000000000000 ) ) ;
#11734=CARTESIAN_POINT ( 'NONE',  ( -38.39232659951203175, 4.291769771411864554, 26.45343327543596956 ) ) ;
#11737=CARTESIAN_POINT ( 'NONE',  ( -19.54308590270338541, -15.50439178786203342, -13.06948577250756927 ) ) ;
#11740=CARTESIAN_POINT ( 'NONE',  ( 21.87349421687013518, -28.05917899276372296, 27.29443387538804444 ) ) ;
#11746=DIRECTION ( 'NONE',  ( 0.000000000000000000, -0.6540809579092761172, -0.7564245504347962834 ) ) ;
#11750=CARTESIAN_POINT ( 'NONE',  ( -15.49969986081099904, 4.873818854044997373, 47.21206422150099513 ) ) ;
#11751=EDGE_CURVE ( 'NONE', #5899, #9493, #9364, .T. ) ;
#11768=AXIS2_PLACEMENT_3D ( 'NONE', #7894, #8902, #13580 ) ;
#11771=VECTOR ( 'NONE', #15062, 1000.000000000000000 ) ;
#11774=ORIENTED_EDGE ( 'NONE', *, *, #4683, .F. ) ;
#11781=DIRECTION ( 'NONE',  ( 0.000000000000000000, 0.000000000000000000, 1.000000000000000000 ) ) ;
#11782=EDGE_LOOP ( 'NONE', ( #6684, #12374, #4671, #6141 ) ) ;
#11787=ORIENTED_EDGE ( 'NONE', *, *, #2519, .F. ) ;
#11795=CARTESIAN_POINT ( 'NONE',  ( 18.17286069890486644, -24.91224770180716419, 7.706609472668462857 ) ) ;
#11798=DIRECTION ( 'NONE',  ( 0.000000000000000000, 0.000000000000000000, 1.000000000000000000 ) ) ;
#11806=CARTESIAN_POINT ( 'NONE',  ( 22.00030013918900096, -27.00737899243800300, 24.21206422150099868 ) ) ;
#11807=EDGE_CURVE ( 'NONE', #609, #970, #6025, .T. ) ;
#11818=CARTESIAN_POINT ( 'NONE',  ( -23.49969986081099904, -19.50737899243800300, 60.84879442494580104 ) ) ;
#11822=AXIS2_PLACEMENT_3D ( 'NONE', #9215, #973, #9142 ) ;
#11823=CARTESIAN_POINT ( 'NONE',  ( -15.49969986081099904, 20.99262100756199700, 47.21206422150099513 ) ) ;
#11836=( BOUNDED_CURVE ( )  B_SPLINE_CURVE ( 3, ( #8777, #9925, #10232, #12307 ),
 .UNSPECIFIED., .F., .T. ) 
 B_SPLINE_CURVE_WITH_KNOTS ( ( 4, 4 ),
 ( 5.074465175390796112, 5.274925224928544765 ),
 .UNSPECIFIED. ) 
 CURVE ( )  GEOMETRIC_REPRESENTATION_ITEM ( )  RATIONAL_B_SPLINE_CURVE ( ( 1.000000000000000000, 0.9966541165307394312, 0.9966541165307394312, 1.000000000000000000 ) ) 
 REPRESENTATION_ITEM ( '' )  );
#11841=CARTESIAN_POINT ( 'NONE',  ( 22.00030013918900096, -27.00737899243800300, 7.712064221501001349 ) ) ;
#11845=FACE_OUTER_BOUND ( 'NONE', #12274, .T. ) ;
#11850=DIRECTION ( 'NONE',  ( 0.000000000000000000, 1.000000000000000000, 1.224646799147350002E-16 ) ) ;
#11852=CARTESIAN_POINT ( 'NONE',  ( 14.77505403666262040, -27.91489101255499250, 2.083060336410837987 ) ) ;
#11859=ORIENTED_EDGE ( 'NONE', *, *, #3283, .F. ) ;
#11861=ORIENTED_EDGE ( 'NONE', *, *, #8170, .F. ) ;
#11864=PLANE ( 'NONE',  #11911 ) ;
#11865=ORIENTED_EDGE ( 'NONE', *, *, #372, .F. ) ;
#11867=CARTESIAN_POINT ( 'NONE',  ( -15.49969986081099904, 10.68321993080349763, 24.21206422150099868 ) ) ;
#11886=CARTESIAN_POINT ( 'NONE',  ( -28.78282149594069850, -32.00737899243799944, 24.21206422150099868 ) ) ;
#11889=DIRECTION ( 'NONE',  ( 0.000000000000000000, -2.185478394931410082E-16, 1.000000000000000000 ) ) ;
#11892=ORIENTED_EDGE ( 'NONE', *, *, #4070, .F. ) ;
#11897=CARTESIAN_POINT ( 'NONE',  ( 21.96544832021356441, -29.82936669528688967, 25.83808190157214568 ) ) ;
#11899=CIRCLE ( 'NONE', #9691, 23.00000000000000000 ) ;
#11906=CARTESIAN_POINT ( 'NONE',  ( 1.760741030006599317, 10.68321993080349763, 16.26994987741148790 ) ) ;
#11910=CARTESIAN_POINT ( 'NONE',  ( -15.49969986081099904, 64.39262100756199914, 29.46206422150100934 ) ) ;
#11911=AXIS2_PLACEMENT_3D ( 'NONE', #10641, #1082, #9415 ) ;
#11915=VERTEX_POINT ( 'NONE', #12258 ) ;
#11918=ORIENTED_EDGE ( 'NONE', *, *, #8188, .T. ) ;
#11926=VECTOR ( 'NONE', #75, 1000.000000000000000 ) ;
#11927=VECTOR ( 'NONE', #3021, 1000.000000000000000 ) ;
#11942=VERTEX_POINT ( 'NONE', #14697 ) ;
#11948=CARTESIAN_POINT ( 'NONE',  ( 0.8003001391889992266, 20.99262100756200056, 16.16206422150100153 ) ) ;
#11951=CARTESIAN_POINT ( 'NONE',  ( -19.97050308595844825, -12.91592837963194462, -13.02052021517568647 ) ) ;
#11953=AXIS2_PLACEMENT_3D ( 'NONE', #6087, #11997, #1281 ) ;
#11959=CARTESIAN_POINT ( 'NONE',  ( 21.85920135429434907, -27.00737899243800300, 20.96206422150100224 ) ) ;
#11976=ORIENTED_EDGE ( 'NONE', *, *, #2230, .F. ) ;
#11978=FACE_OUTER_BOUND ( 'NONE', #5919, .T. ) ;
#11980=ORIENTED_EDGE ( 'NONE', *, *, #13468, .F. ) ;
#11992=CIRCLE ( 'NONE', #9071, 5.000000000000000000 ) ;
#11994=DIRECTION ( 'NONE',  ( 1.000000000000000000, 0.000000000000000000, 0.000000000000000000 ) ) ;
#11995=FACE_OUTER_BOUND ( 'NONE', #1556, .T. ) ;
#11997=DIRECTION ( 'NONE',  ( 0.000000000000000000, 1.000000000000000000, 1.224646799147350002E-16 ) ) ;
#12005=ADVANCED_FACE ( 'NONE', ( #1148, #1079 ), #12639, .T. ) ;
#12006=DIRECTION ( 'NONE',  ( 0.000000000000000000, 0.000000000000000000, 1.000000000000000000 ) ) ;
#12008=CARTESIAN_POINT ( 'NONE',  ( 18.52099659588564862, -27.46909528396324518, 8.437240866514711612 ) ) ;
#12015=CARTESIAN_POINT ( 'NONE',  ( 2.237328452597175499, 7.708027139131397476, 31.02581378992296735 ) ) ;
#12017=DIRECTION ( 'NONE',  ( -1.000000000000000000, 0.000000000000000000, 0.000000000000000000 ) ) ;
#12023=CARTESIAN_POINT ( 'NONE',  ( -15.49969986081099904, 20.99262100756200056, 24.21206422150099868 ) ) ;
#12026=DIRECTION ( 'NONE',  ( 0.000000000000000000, 1.000000000000000000, 1.224646799147350002E-16 ) ) ;
#12029=CYLINDRICAL_SURFACE ( 'NONE', #6885, 2.500000000000002220 ) ;
#12030=AXIS2_PLACEMENT_3D ( 'NONE', #4889, #9542, #12075 ) ;
#12032=AXIS2_PLACEMENT_3D ( 'NONE', #10621, #1365, #13915 ) ;
#12033=ORIENTED_EDGE ( 'NONE', *, *, #7434, .T. ) ;
#12038=VECTOR ( 'NONE', #8550, 1000.000000000000000 ) ;
#12044=EDGE_CURVE ( 'NONE', #2383, #11942, #11036, .T. ) ;
#12055=CARTESIAN_POINT ( 'NONE',  ( -15.49969986081099904, 37.56536188261469533, 24.21206422150100224 ) ) ;
#12059=ORIENTED_EDGE ( 'NONE', *, *, #2403, .F. ) ;
#12066=DIRECTION ( 'NONE',  ( 0.000000000000000000, 0.000000000000000000, 1.000000000000000000 ) ) ;
#12069=DIRECTION ( 'NONE',  ( 0.000000000000000000, 1.000000000000000000, 1.224646799147350002E-16 ) ) ;
#12075=DIRECTION ( 'NONE',  ( 0.000000000000000000, 1.224646799147350002E-16, -1.000000000000000000 ) ) ;
#12085=CARTESIAN_POINT ( 'NONE',  ( 14.70471644742069373, -27.47017211369107770, 1.987150903830744664 ) ) ;
#12101=CARTESIAN_POINT ( 'NONE',  ( -14.84599537932207802, -3.507399398443247662, 61.71206405750629642 ) ) ;
#12113=CARTESIAN_POINT ( 'NONE',  ( 7.200737182676100190, 4.873818854045000037, 27.91208557747711083 ) ) ;
#12117=CARTESIAN_POINT ( 'NONE',  ( -38.36664365575047952, 4.365428709180945610, 21.66608770973884646 ) ) ;
#12118=ADVANCED_FACE ( 'NONE', ( #1459 ), #88, .T. ) ;
#12119=CARTESIAN_POINT ( 'NONE',  ( -15.49969986081099904, 70.89785811302749607, 24.21206422150100579 ) ) ;
#12120=CARTESIAN_POINT ( 'NONE',  ( -35.91308956371933192, 5.973563155936505886, 18.89224887993488977 ) ) ;
#12130=CARTESIAN_POINT ( 'NONE',  ( 4.893136743221020879, 5.983413651705625114, 18.88106025385081566 ) ) ;
#12142=CARTESIAN_POINT ( 'NONE',  ( 21.98622857737163727, -23.92291445542225858, 23.16614582331327554 ) ) ;
#12143=ORIENTED_EDGE ( 'NONE', *, *, #8205, .F. ) ;
#12148=DIRECTION ( 'NONE',  ( 0.000000000000000000, 0.000000000000000000, 1.000000000000000000 ) ) ;
#12151=CARTESIAN_POINT ( 'NONE',  ( 17.94160745424604642, -29.55396020057183648, 7.242669092553135179 ) ) ;
#12156=EDGE_CURVE ( 'NONE', #10535, #11202, #92, .T. ) ;
#12166=VECTOR ( 'NONE', #9179, 1000.000000000000000 ) ;
#12169=CARTESIAN_POINT ( 'NONE',  ( -33.01292635343269666, 8.758714366253697037, 16.84401747001000160 ) ) ;
#12173=AXIS2_PLACEMENT_3D ( 'NONE', #11510, #4479, #9133 ) ;
#12179=DIRECTION ( 'NONE',  ( 0.000000000000000000, 9.130123557772668334E-17, -1.000000000000000000 ) ) ;
#12180=ORIENTED_EDGE ( 'NONE', *, *, #4388, .F. ) ;
#12182=EDGE_LOOP ( 'NONE', ( #3035, #11918 ) ) ;
#12188=CIRCLE ( 'NONE', #9237, 3.250000000000002665 ) ;
#12189=EDGE_CURVE ( 'NONE', #11256, #3447, #1053, .T. ) ;
#12191=CARTESIAN_POINT ( 'NONE',  ( 13.85920135429429934, -27.00737899243800300, 39.96206422150099513 ) ) ;
#12197=CARTESIAN_POINT ( 'NONE',  ( 9.000300139189000959, -32.00737899243799944, 24.21206422150099868 ) ) ;
#12199=DIRECTION ( 'NONE',  ( 0.000000000000000000, 0.000000000000000000, 1.000000000000000000 ) ) ;
#12202=LINE ( 'NONE', #8745, #1279 ) ;
#12203=CARTESIAN_POINT ( 'NONE',  ( -15.49969986081099904, 22.99262100756200056, 24.21206422150100224 ) ) ;
#12208=CARTESIAN_POINT ( 'NONE',  ( -15.49969986081099727, 71.39262100756199914, 32.52626782222684909 ) ) ;
#12211=CIRCLE ( 'NONE', #8292, 15.62500000000000000 ) ;
#12212=DIRECTION ( 'NONE',  ( 1.000000000000000000, 0.000000000000000000, 0.000000000000000000 ) ) ;
#12213=CARTESIAN_POINT ( 'NONE',  ( -2.216578225681298697, -31.14135358865350511, -123.9247733198440073 ) ) ;
#12220=CARTESIAN_POINT ( 'NONE',  ( 22.00030675015428727, -23.75730271206433386, 24.00114908445582529 ) ) ;
#12226=B_SPLINE_CURVE_WITH_KNOTS ( 'NONE', 3,
 ( #26, #9499, #11951, #8191, #4919, #3612, #2691, #14172, #13108, #4994, #5892, #4764, #9653, #14324, #331, #9421, #3836, #6042 ),
 .UNSPECIFIED., .F., .F.,
 ( 4, 2, 2, 2, 2, 2, 2, 2, 4 ),
 ( 0.000000000000000000, 0.0008864497783454140366, 0.001772899556690828073, 0.002659349335036241893, 0.003545799113381656147, 0.004432248891727070400, 0.005318698670072483786, 0.006205148448417898040, 0.007091598226763312293 ),
 .UNSPECIFIED. ) ;
#12228=DIRECTION ( 'NONE',  ( 0.000000000000000000, 0.000000000000000000, -1.000000000000000000 ) ) ;
#12230=CARTESIAN_POINT ( 'NONE',  ( -15.49969986081099904, 71.39262100756199914, 24.21206422150100579 ) ) ;
#12233=DIRECTION ( 'NONE',  ( 0.000000000000000000, 1.224646799147350002E-16, -1.000000000000000000 ) ) ;
#12234=ORIENTED_EDGE ( 'NONE', *, *, #6951, .T. ) ;
#12240=VERTEX_POINT ( 'NONE', #14758 ) ;
#12242=CARTESIAN_POINT ( 'NONE',  ( -2.216578225681298697, -31.14135358865360104, 59.28069236156870403 ) ) ;
#12246=ADVANCED_FACE ( 'NONE', ( #9792 ), #3979, .T. ) ;
#12249=DIRECTION ( 'NONE',  ( 0.000000000000000000, 0.000000000000000000, -1.000000000000000000 ) ) ;
#12258=CARTESIAN_POINT ( 'NONE',  ( -15.49969986081099904, 71.39262100756199914, 15.89786062077516782 ) ) ;
#12262=FACE_OUTER_BOUND ( 'NONE', #8830, .T. ) ;
#12265=CARTESIAN_POINT ( 'NONE',  ( -13.50277480631462979, -9.463945884570895473, -13.23572242406894617 ) ) ;
#12270=VECTOR ( 'NONE', #2906, 1000.000000000000000 ) ;
#12271=VECTOR ( 'NONE', #12376, 1000.000000000000000 ) ;
#12274=EDGE_LOOP ( 'NONE', ( #8540, #416, #14983, #5348, #11314, #1047, #11268, #9276, #3048 ) ) ;
#12278=VERTEX_POINT ( 'NONE', #4358 ) ;
#12279=ORIENTED_EDGE ( 'NONE', *, *, #14636, .F. ) ;
#12280=CARTESIAN_POINT ( 'NONE',  ( 21.85920135429435263, -27.21949063834600935, 20.96206422150100224 ) ) ;
#12281=EDGE_CURVE ( 'NONE', #2152, #4803, #2543, .T. ) ;
#12282=CARTESIAN_POINT ( 'NONE',  ( -15.49969986081099904, 7.183219930803497633, 24.21206422150099868 ) ) ;
#12287=CARTESIAN_POINT ( 'NONE',  ( 4.742609669324512112, 6.055639158887895945, 18.80100070848684624 ) ) ;
#12289=DIRECTION ( 'NONE',  ( -1.224646799147350002E-16, -1.224646799147350002E-16, 1.000000000000000000 ) ) ;
#12292=ORIENTED_EDGE ( 'NONE', *, *, #11117, .F. ) ;
#12294=ADVANCED_FACE ( 'NONE', ( #8934 ), #5642, .F. ) ;
#12302=CARTESIAN_POINT ( 'NONE',  ( -35.49969986081099904, -19.50737899243800300, -7.509379629622798369 ) ) ;
#12307=CARTESIAN_POINT ( 'NONE',  ( 4.500300139189000959, -19.50737899243801010, -7.509379629622798369 ) ) ;
#12309=CARTESIAN_POINT ( 'NONE',  ( -32.93478177869805279, 9.209028802409704895, 31.76314389137934668 ) ) ;
#12311=EDGE_CURVE ( 'NONE', #9278, #13407, #6856, .T. ) ;
#12313=DIRECTION ( 'NONE',  ( 0.000000000000000000, 1.850371707708594316E-16, -1.000000000000000000 ) ) ;
#12318=ORIENTED_EDGE ( 'NONE', *, *, #6744, .F. ) ;
#12321=LINE ( 'NONE', #11471, #3294 ) ;
#12322=AXIS2_PLACEMENT_3D ( 'NONE', #7289, #9518, #14189 ) ;
#12323=DIRECTION ( 'NONE',  ( -2.526242637138179679E-48, -1.000000000000000000, -1.224646799147350002E-16 ) ) ;
#12333=VERTEX_POINT ( 'NONE', #7849 ) ;
#12352=ORIENTED_EDGE ( 'NONE', *, *, #1799, .F. ) ;
#12353=ORIENTED_EDGE ( 'NONE', *, *, #2073, .T. ) ;
#12358=CARTESIAN_POINT ( 'NONE',  ( 4.814653393906814571, 6.021066563893142209, 18.83900906337587600 ) ) ;
#12359=DIRECTION ( 'NONE',  ( 0.000000000000000000, 0.000000000000000000, -1.000000000000000000 ) ) ;
#12362=DIRECTION ( 'NONE',  ( 0.000000000000000000, -1.000000000000000000, -1.224646799147350002E-16 ) ) ;
#12366=EDGE_CURVE ( 'NONE', #11542, #10768, #11568, .T. ) ;
#12369=CARTESIAN_POINT ( 'NONE',  ( 2.054681262915651008, 8.544173770627839559, 31.48152205384135982 ) ) ;
#12370=EDGE_CURVE ( 'NONE', #10814, #1247, #4892, .T. ) ;
#12374=ORIENTED_EDGE ( 'NONE', *, *, #6574, .T. ) ;
#12376=DIRECTION ( 'NONE',  ( 0.000000000000000000, 1.000000000000000000, 1.224646799147350002E-16 ) ) ;
#12386=VERTEX_POINT ( 'NONE', #2665 ) ;
#12397=CARTESIAN_POINT ( 'NONE',  ( -6.394347403426568377, -9.362396602573261006, 60.59006687612484399 ) ) ;
#12399=AXIS2_PLACEMENT_3D ( 'NONE', #1598, #312, #7174 ) ;
#12404=CARTESIAN_POINT ( 'NONE',  ( 14.68618260102870288, -27.24056927272615880, 46.46206422150100224 ) ) ;
#12407=ORIENTED_EDGE ( 'NONE', *, *, #13372, .T. ) ;
#12419=DIRECTION ( 'NONE',  ( 0.000000000000000000, 0.000000000000000000, 1.000000000000000000 ) ) ;
#12424=CARTESIAN_POINT ( 'NONE',  ( 18.35357463111971654, -25.46302391628681505, 40.34329577599203276 ) ) ;
#12433=DIRECTION ( 'NONE',  ( 1.000000000000000000, 0.000000000000000000, 0.000000000000000000 ) ) ;
#12438=CARTESIAN_POINT ( 'NONE',  ( 9.000300139189000959, -32.00737899243799944, -4.178074911655800250 ) ) ;
#12440=CARTESIAN_POINT ( 'NONE',  ( 4.917000788749030349, 5.971976172174768394, 29.53007407726659750 ) ) ;
#12445=ORIENTED_EDGE ( 'NONE', *, *, #14784, .F. ) ;
#12456=EDGE_CURVE ( 'NONE', #6725, #15087, #13001, .T. ) ;
#12460=CYLINDRICAL_SURFACE ( 'NONE', #6726, 3.249999999999999556 ) ;
#12465=VERTEX_POINT ( 'NONE', #9545 ) ;
#12475=B_SPLINE_CURVE_WITH_KNOTS ( 'NONE', 3,
 ( #6503, #4073, #10028, #13490, #11113, #12265, #5296, #5147, #634, #6433, #10967, #4153, #2930, #7658, #4001, #8660, #8886, #1857 ),
 .UNSPECIFIED., .F., .F.,
 ( 4, 2, 2, 2, 2, 2, 2, 2, 4 ),
 ( 0.007091598226763312293, 0.007978859691346384259, 0.008866121155929454489, 0.009753382620512526455, 0.01064064408509559842, 0.01152790554967867039, 0.01241516701426174235, 0.01330242847884481258, 0.01418968994342788455 ),
 .UNSPECIFIED. ) ;
#12481=CARTESIAN_POINT ( 'NONE',  ( 17.85288399792872127, -29.68312937030077236, 41.35546770520703319 ) ) ;
#12495=CARTESIAN_POINT ( 'NONE',  ( 17.02925260421022813, -23.75019164044109132, 42.87573938909707039 ) ) ;
#12498=VERTEX_POINT ( 'NONE', #10776 ) ;
#12502=ORIENTED_EDGE ( 'NONE', *, *, #7374, .T. ) ;
#12508=PLANE ( 'NONE',  #1424 ) ;
#12511=CARTESIAN_POINT ( 'NONE',  ( 4.926418148162898802, 5.967462257416214833, 29.52493280993808966 ) ) ;
#12513=DIRECTION ( 'NONE',  ( 0.000000000000000000, -1.000000000000000000, -1.224646799147350002E-16 ) ) ;
#12522=CYLINDRICAL_SURFACE ( 'NONE', #11822, 10.00000000000000000 ) ;
#12523=ORIENTED_EDGE ( 'NONE', *, *, #14266, .T. ) ;
#12526=AXIS2_PLACEMENT_3D ( 'NONE', #9240, #1135, #13920 ) ;
#12534=FACE_OUTER_BOUND ( 'NONE', #11726, .T. ) ;
#12545=ORIENTED_EDGE ( 'NONE', *, *, #847, .F. ) ;
#12547=B_SPLINE_CURVE_WITH_KNOTS ( 'NONE', 3,
 ( #813, #10129, #8366, #14112 ),
 .UNSPECIFIED., .F., .F.,
 ( 4, 4 ),
 ( 0.01169941957287879905, 0.01381006638855979997 ),
 .UNSPECIFIED. ) ;
#12555=CARTESIAN_POINT ( 'NONE',  ( -8.200120392665880331, -6.662954729433940848, 60.99550424616020194 ) ) ;
#12564=CARTESIAN_POINT ( 'NONE',  ( -25.16886795621463691, -10.89431112827525361, 60.44430563842290383 ) ) ;
#12569=VERTEX_POINT ( 'NONE', #14440 ) ;
#12579=ORIENTED_EDGE ( 'NONE', *, *, #4551, .T. ) ;
#12580=CARTESIAN_POINT ( 'NONE',  ( 15.03590892877081409, -25.29102231028643644, 45.98015512529381965 ) ) ;
#12596=CARTESIAN_POINT ( 'NONE',  ( 4.527565447144258570, 6.159096188232942914, 29.73988678045787637 ) ) ;
#12599=CARTESIAN_POINT ( 'NONE',  ( -19.99969986081099904, -13.50737899243800122, -13.01695671647154917 ) ) ;
#12607=CARTESIAN_POINT ( 'NONE',  ( 0.8003001391889992266, 3.992621007561997892, 24.26206422150100295 ) ) ;
#12609=CARTESIAN_POINT ( 'NONE',  ( 6.045543233663400073, 12.99262100756199878, 16.16206422150100153 ) ) ;
#12613=AXIS2_PLACEMENT_3D ( 'NONE', #9446, #3637, #8369 ) ;
#12617=CARTESIAN_POINT ( 'NONE',  ( -35.90489723645450226, 5.977487861575448314, 29.53635566902382337 ) ) ;
#12629=CARTESIAN_POINT ( 'NONE',  ( -6.020613275810588583, -10.26707144315182063, 60.49515945283604879 ) ) ;
#12634=EDGE_LOOP ( 'NONE', ( #12445, #14305, #5236, #5005 ) ) ;
#12636=CIRCLE ( 'NONE', #1136, 2.499999999999998668 ) ;
#12637=ORIENTED_EDGE ( 'NONE', *, *, #6696, .T. ) ;
#12639=PLANE ( 'NONE',  #1545 ) ;
#12642=ORIENTED_EDGE ( 'NONE', *, *, #14726, .F. ) ;
#12644=ORIENTED_EDGE ( 'NONE', *, *, #181, .T. ) ;
#12645=( GEOMETRIC_REPRESENTATION_CONTEXT ( 3 ) GLOBAL_UNCERTAINTY_ASSIGNED_CONTEXT ( ( #6597 ) ) GLOBAL_UNIT_ASSIGNED_CONTEXT ( ( #9580, #3772, #12966 ) ) REPRESENTATION_CONTEXT ( 'NONE', 'WORKASPACE' ) );
#12647=AXIS2_PLACEMENT_3D ( 'NONE', #10688, #10771, #14289 ) ;
#12657=CARTESIAN_POINT ( 'NONE',  ( 17.66731393161950336, -24.11684619341258085, 41.71177241952297265 ) ) ;
#12658=ORIENTED_EDGE ( 'NONE', *, *, #14408, .F. ) ;
#12659=VERTEX_POINT ( 'NONE', #5704 ) ;
#12660=EDGE_LOOP ( 'NONE', ( #9393, #13709, #1557, #13629, #7278, #10654, #29, #10443 ) ) ;
#12661=ORIENTED_EDGE ( 'NONE', *, *, #14125, .T. ) ;
#12669=CARTESIAN_POINT ( 'NONE',  ( 4.795664383891133475, 6.030134292646086358, 29.59621904580064822 ) ) ;
#12676=FACE_OUTER_BOUND ( 'NONE', #133, .T. ) ;
#12682=VECTOR ( 'NONE', #12828, 1000.000000000000000 ) ;
#12685=CIRCLE ( 'NONE', #713, 37.50000000000000000 ) ;
#12686=PRODUCT_DEFINITION_FORMATION_WITH_SPECIFIED_SOURCE ( 'ANY', '', #10923, .NOT_KNOWN. ) ;
#12693=CARTESIAN_POINT ( 'NONE',  ( -15.49969986081079654, 1010.738102757666070, -1640.067418128998952 ) ) ;
#12697=ADVANCED_FACE ( 'NONE', ( #4417 ), #12522, .F. ) ;
#12700=CIRCLE ( 'NONE', #1457, 23.00000000000000000 ) ;
#12702=EDGE_CURVE ( 'NONE', #6219, #1569, #11224, .T. ) ;
#12706=CARTESIAN_POINT ( 'NONE',  ( 9.000300139189000959, -27.00737899243800300, 2.712064221501000461 ) ) ;
#12707=DIRECTION ( 'NONE',  ( 3.202566417187950042E-16, 1.224646799147350002E-16, -1.000000000000000000 ) ) ;
#12708=CARTESIAN_POINT ( 'NONE',  ( -35.49969986081099904, -19.50737899243800300, 55.93350807262480373 ) ) ;
#12715=ORIENTED_EDGE ( 'NONE', *, *, #6382, .F. ) ;
#12718=AXIS2_PLACEMENT_3D ( 'NONE', #39, #8206, #3551 ) ;
#12720=EDGE_CURVE ( 'NONE', #364, #5054, #7176, .T. ) ;
#12724=LINE ( 'NONE', #8889, #9403 ) ;
#12727=VECTOR ( 'NONE', #9571, 1000.000000000000000 ) ;
#12728=ORIENTED_EDGE ( 'NONE', *, *, #13939, .F. ) ;
#12734=ORIENTED_EDGE ( 'NONE', *, *, #372, .T. ) ;
#12735=EDGE_LOOP ( 'NONE', ( #4148, #12642, #14938, #5513 ) ) ;
#12742=DIRECTION ( 'NONE',  ( 0.000000000000000000, 1.000000000000000000, 1.224646799147350002E-16 ) ) ;
#12748=ORIENTED_EDGE ( 'NONE', *, *, #13468, .T. ) ;
#12751=ORIENTED_EDGE ( 'NONE', *, *, #1737, .F. ) ;
#12753=CARTESIAN_POINT ( 'NONE',  ( -15.49969986081099904, 22.99262100756200056, 24.21206422150100224 ) ) ;
#12755=DIRECTION ( 'NONE',  ( 0.000000000000000000, 0.000000000000000000, 1.000000000000000000 ) ) ;
#12768=DIRECTION ( 'NONE',  ( 0.000000000000000000, 1.000000000000000000, 1.224646799147350002E-16 ) ) ;
#12773=CARTESIAN_POINT ( 'NONE',  ( -35.31162891843938922, 6.261951257131300963, 29.84176477860722443 ) ) ;
#12775=AXIS2_PLACEMENT_3D ( 'NONE', #3166, #876, #5457 ) ;
#12787=CARTESIAN_POINT ( 'NONE',  ( -5.542205825327698676, -14.57691648049767963, 60.36598623123717999 ) ) ;
#12797=CARTESIAN_POINT ( 'NONE',  ( -19.34548696706897175, -4.262109752139091157, 61.51804659027894928 ) ) ;
#12801=DIRECTION ( 'NONE',  ( 0.000000000000000000, 0.000000000000000000, -1.000000000000000000 ) ) ;
#12814=AXIS2_PLACEMENT_3D ( 'NONE', #11683, #12362, #2873 ) ;
#12821=DIRECTION ( 'NONE',  ( 1.000000000000000000, 0.000000000000000000, 0.000000000000000000 ) ) ;
#12828=DIRECTION ( 'NONE',  ( -7.070501591499380254E-17, -1.224646799147350002E-16, 1.000000000000000000 ) ) ;
#12839=VERTEX_POINT ( 'NONE', #4300 ) ;
#12840=CARTESIAN_POINT ( 'NONE',  ( -15.49969986081099371, -19.50737899243800300, -13.28793577849899599 ) ) ;
#12847=ORIENTED_EDGE ( 'NONE', *, *, #4306, .F. ) ;
#12853=DIRECTION ( 'NONE',  ( -1.000000000000000000, 0.000000000000000000, 0.000000000000000000 ) ) ;
#12857=ADVANCED_FACE ( 'NONE', ( #3149 ), #1500, .F. ) ;
#12870=DIRECTION ( 'NONE',  ( 0.000000000000000000, 1.000000000000000000, 1.224646799147350002E-16 ) ) ;
#12878=CARTESIAN_POINT ( 'NONE',  ( 18.52103932491873195, -26.54644467364772709, 8.437333501280610548 ) ) ;
#12880=CYLINDRICAL_SURFACE ( 'NONE', #2301, 5.250000000000000888 ) ;
#12882=CARTESIAN_POINT ( 'NONE',  ( -12.52737422752994156, -16.89904518643017894, -13.17054741830957987 ) ) ;
#12883=ORIENTED_EDGE ( 'NONE', *, *, #7924, .F. ) ;
#12884=VERTEX_POINT ( 'NONE', #8530 ) ;
#12896=AXIS2_PLACEMENT_3D ( 'NONE', #9620, #14438, #6387 ) ;
#12904=CARTESIAN_POINT ( 'NONE',  ( -15.49969986081099371, -18.00737899243799944, -13.28793577849899776 ) ) ;
#12907=CARTESIAN_POINT ( 'NONE',  ( 21.89440327984462442, -28.63919800004179095, 27.03079604377302303 ) ) ;
#12913=EDGE_CURVE ( 'NONE', #6353, #5152, #15011, .T. ) ;
#12916=ADVANCED_FACE ( 'NONE', ( #12262 ), #5440, .F. ) ;
#12920=EDGE_CURVE ( 'NONE', #9493, #6681, #14354, .T. ) ;
#12924=CARTESIAN_POINT ( 'NONE',  ( -25.49969986081099904, -13.50737899243799944, 6.712064221500998684 ) ) ;
#12926=ORIENTED_EDGE ( 'NONE', *, *, #10435, .F. ) ;
#12931=VERTEX_POINT ( 'NONE', #9860 ) ;
#12934=ADVANCED_FACE ( 'NONE', ( #12961 ), #12880, .F. ) ;
#12937=B_SPLINE_CURVE_WITH_KNOTS ( 'NONE', 3,
 ( #14416, #9673, #6218, #10898, #10971, #3934, #567, #425, #2787, #5232, #4010, #7442, #5303, #11121, #12120, #9895, #14638, #14563, #6293, #641 ),
 .UNSPECIFIED., .F., .F.,
 ( 4, 2, 2, 1, 1, 1, 1, 1, 1, 2, 2, 2, 4 ),
 ( 0.000000000000000000, 0.2500000000006495915, 0.3750000000009743872, 0.4375000000011352030, 0.4687500000012148060, 0.4843750000012558843, 0.4921875000012767565, 0.4960937500012871371, 0.4980468750012915224, 0.4990234375012933543, 0.5000000000012951862, 0.7500000000006475931, 1.000000000000000000 ),
 .UNSPECIFIED. ) ;
#12941=FACE_BOUND ( 'NONE', #6737, .T. ) ;
#12952=VERTEX_POINT ( 'NONE', #179 ) ;
#12953=AXIS2_PLACEMENT_3D ( 'NONE', #9218, #4646, #4420 ) ;
#12954=DIRECTION ( 'NONE',  ( 0.000000000000000000, -1.000000000000000000, -1.224646799147350002E-16 ) ) ;
#12961=FACE_OUTER_BOUND ( 'NONE', #5311, .T. ) ;
#12963=DIRECTION ( 'NONE',  ( -1.927249326158839857E-15, 1.000000000000000000, 0.000000000000000000 ) ) ;
#12964=CARTESIAN_POINT ( 'NONE',  ( -11.22942933597135706, -14.95710884211384695, -13.04417926711732356 ) ) ;
#12966=( NAMED_UNIT ( * ) SI_UNIT ( $, .STERADIAN. ) SOLID_ANGLE_UNIT ( ) );
#12970=EDGE_LOOP ( 'NONE', ( #5058, #8043, #2339, #8728 ) ) ;
#12973=CARTESIAN_POINT ( 'NONE',  ( 22.00030013918900096, -27.00737899243800300, 43.21206422150100224 ) ) ;
#12976=EDGE_CURVE ( 'NONE', #6551, #15009, #13317, .T. ) ;
#12978=DIRECTION ( 'NONE',  ( 0.000000000000000000, 1.000000000000000000, 1.224646799147350002E-16 ) ) ;
#12994=VERTEX_POINT ( 'NONE', #5191 ) ;
#13001=LINE ( 'NONE', #11841, #6912 ) ;
#13004=CARTESIAN_POINT ( 'NONE',  ( 1.760741030006599317, 10.68321993080349763, 32.15417856559049881 ) ) ;
#13008=DIRECTION ( 'NONE',  ( 0.000000000000000000, 1.224646799147350002E-16, -1.000000000000000000 ) ) ;
#13010=CARTESIAN_POINT ( 'NONE',  ( -6.194530427787681148, -17.17519237421424094, 60.53940394396870062 ) ) ;
#13014=AXIS2_PLACEMENT_3D ( 'NONE', #3965, #1367, #13008 ) ;
#13015=CARTESIAN_POINT ( 'NONE',  ( 16.67641871555605348, -30.25287370156248912, 4.950703260674607975 ) ) ;
#13028=DIRECTION ( 'NONE',  ( 1.000000000000000000, 1.499759782661853776E-32, -1.224646799147353207E-16 ) ) ;
#13030=AXIS2_PLACEMENT_3D ( 'NONE', #3110, #11150, #14668 ) ;
#13050=DIRECTION ( 'NONE',  ( 0.000000000000000000, 1.224646799147350002E-16, -1.000000000000000000 ) ) ;
#13051=VECTOR ( 'NONE', #14040, 1000.000000000000000 ) ;
#13053=FACE_OUTER_BOUND ( 'NONE', #10526, .T. ) ;
#13058=EDGE_LOOP ( 'NONE', ( #9175, #3355 ) ) ;
#13062=ORIENTED_EDGE ( 'NONE', *, *, #14726, .T. ) ;
#13064=VECTOR ( 'NONE', #15051, 1000.000000000000114 ) ;
#13068=CYLINDRICAL_SURFACE ( 'NONE', #10202, 3.250000000000002665 ) ;
#13069=DIRECTION ( 'NONE',  ( 0.000000000000000000, -1.000000000000000000, -1.224646799147350002E-16 ) ) ;
#13077=ORIENTED_EDGE ( 'NONE', *, *, #9667, .F. ) ;
#13080=AXIS2_PLACEMENT_3D ( 'NONE', #4589, #2371, #155 ) ;
#13094=ORIENTED_EDGE ( 'NONE', *, *, #6545, .F. ) ;
#13101=EDGE_CURVE ( 'NONE', #11705, #3567, #11836, .T. ) ;
#13108=CARTESIAN_POINT ( 'NONE',  ( -18.88793338163855751, -10.53151576015236657, -13.13513322929154725 ) ) ;
#13111=APPLICATION_CONTEXT ( 'automotive_design' ) ;
#13112=CARTESIAN_POINT ( 'NONE',  ( -11.14430855146604316, -14.67662645734702842, -13.03419638460520069 ) ) ;
#13118=ORIENTED_EDGE ( 'NONE', *, *, #8128, .T. ) ;
#13121=DIRECTION ( 'NONE',  ( 0.000000000000000000, 0.000000000000000000, 1.000000000000000000 ) ) ;
#13126=DIRECTION ( 'NONE',  ( 0.000000000000000000, 1.000000000000000000, 1.224646799147350002E-16 ) ) ;
#13128=MECHANICAL_DESIGN_GEOMETRIC_PRESENTATION_REPRESENTATION('',(#7235),#12645);
#13134=CARTESIAN_POINT ( 'NONE',  ( -32.76014075162859740, 10.68321993080349763, 32.15417856559049881 ) ) ;
#13139=CONICAL_SURFACE ( 'NONE', #15063, 8.314203600725839749, 0.8578293273552097808 ) ;
#13144=DIRECTION ( 'NONE',  ( 0.000000000000000000, 1.508455196501571429E-16, -1.000000000000000000 ) ) ;
#13145=CIRCLE ( 'NONE', #5312, 37.50000000000000000 ) ;
#13146=CYLINDRICAL_SURFACE ( 'NONE', #5038, 6.250000000000001776 ) ;
#13148=AXIS2_PLACEMENT_3D ( 'NONE', #4605, #12954, #15078 ) ;
#13152=ORIENTED_EDGE ( 'NONE', *, *, #9575, .F. ) ;
#13154=CARTESIAN_POINT ( 'NONE',  ( -31.79969986081099975, 11.99262100756199878, 24.26206422150100650 ) ) ;
#13162=VECTOR ( 'NONE', #7641, 1000.000000000000000 ) ;
#13165=CARTESIAN_POINT ( 'NONE',  ( 15.51501874267047576, -29.51299105794866051, 3.131973333163219131 ) ) ;
#13186=DIRECTION ( 'NONE',  ( 0.000000000000000000, 0.000000000000000000, 1.000000000000000000 ) ) ;
#13192=DIRECTION ( 'NONE',  ( 0.000000000000000000, 0.000000000000000000, 1.000000000000000000 ) ) ;
#13200=VECTOR ( 'NONE', #7801, 1000.000000000000000 ) ;
#13201=EDGE_CURVE ( 'NONE', #12931, #7197, #13755, .T. ) ;
#13214=VERTEX_POINT ( 'NONE', #3422 ) ;
#13217=CARTESIAN_POINT ( 'NONE',  ( 1.935382057079082951, 9.209028802368010247, 16.66098455162964953 ) ) ;
#13218=CIRCLE ( 'NONE', #11246, 15.87500000000000355 ) ;
#13219=DIRECTION ( 'NONE',  ( 0.000000000000000000, 1.224646799147350002E-16, -1.000000000000000000 ) ) ;
#13223=AXIS2_PLACEMENT_3D ( 'NONE', #4762, #10495, #8111 ) ;
#13236=EDGE_CURVE ( 'NONE', #11256, #11705, #11607, .T. ) ;
#13239=CARTESIAN_POINT ( 'NONE',  ( 14.68618260102867445, -27.23672126206158239, 1.962064221501001571 ) ) ;
#13240=CARTESIAN_POINT ( 'NONE',  ( -15.49969986081099904, 37.56536188261469533, 24.21206422150100224 ) ) ;
#13245=VERTEX_POINT ( 'NONE', #11750 ) ;
#13253=AXIS2_PLACEMENT_3D ( 'NONE', #10118, #1025, #14943 ) ;
#13254=CARTESIAN_POINT ( 'NONE',  ( -33.14240505666059988, 8.120575443056504028, 17.15924262193565397 ) ) ;
#13256=EDGE_CURVE ( 'NONE', #11290, #12569, #8233, .T. ) ;
#13257=CARTESIAN_POINT ( 'NONE',  ( -11.06429811985332279, -4.540650544146559220, 61.44996607439977510 ) ) ;
#13265=ORIENTED_EDGE ( 'NONE', *, *, #5507, .T. ) ;
#13270=VERTEX_POINT ( 'NONE', #142 ) ;
#13275=VECTOR ( 'NONE', #9904, 1000.000000000000000 ) ;
#13294=DIRECTION ( 'NONE',  ( 0.000000000000000000, -2.220446049250312588E-16, 1.000000000000000000 ) ) ;
#13296=EDGE_CURVE ( 'NONE', #12386, #2212, #11731, .T. ) ;
#13304=DIRECTION ( 'NONE',  ( 1.000000000000000000, 0.000000000000000000, 0.000000000000000000 ) ) ;
#13305=VERTEX_POINT ( 'NONE', #6993 ) ;
#13306=CARTESIAN_POINT ( 'NONE',  ( 21.91135930735600468, -25.02476975920917113, 21.62815801113326941 ) ) ;
#13316=CARTESIAN_POINT ( 'NONE',  ( 15.03585100355005189, -28.72364914449597251, 2.443890032762031872 ) ) ;
#13317=LINE ( 'NONE', #5119, #9385 ) ;
#13319=CARTESIAN_POINT ( 'NONE',  ( -32.89917128247499534, 9.436645346093119002, 31.84501495524920500 ) ) ;
#13323=ORIENTED_EDGE ( 'NONE', *, *, #5891, .F. ) ;
#13327=EDGE_CURVE ( 'NONE', #259, #14313, #5723, .T. ) ;
#13333=CARTESIAN_POINT ( 'NONE',  ( -9.394734159045251332, -5.558363548092267514, 61.21584039466183924 ) ) ;
#13346=CIRCLE ( 'NONE', #12613, 5.250000000000000888 ) ;
#13350=DIRECTION ( 'NONE',  ( 0.000000000000000000, 1.000000000000000000, 1.224646799147350002E-16 ) ) ;
#13352=EDGE_LOOP ( 'NONE', ( #360, #4204 ) ) ;
#13356=DIRECTION ( 'NONE',  ( 0.000000000000000000, 1.369518533665900312E-16, -1.000000000000000000 ) ) ;
#13360=LINE ( 'NONE', #12208, #5971 ) ;
#13365=ORIENTED_EDGE ( 'NONE', *, *, #5998, .F. ) ;
#13371=CARTESIAN_POINT ( 'NONE',  ( 21.85920135429435263, -27.00737899243800300, 27.46206422150099868 ) ) ;
#13372=EDGE_CURVE ( 'NONE', #14381, #3567, #13520, .T. ) ;
#13375=VERTEX_POINT ( 'NONE', #7152 ) ;
#13376=CIRCLE ( 'NONE', #9193, 19.00000000000000000 ) ;
#13378=PRODUCT_DEFINITION_SHAPE ( 'NONE', 'NONE',  #9473 ) ;
#13381=CARTESIAN_POINT ( 'NONE',  ( 22.00030013918900096, -27.00737899243800300, 43.21206422150100224 ) ) ;
#13388=CARTESIAN_POINT ( 'NONE',  ( -15.49969986081099904, -19.50737899243800300, 24.21206422150100224 ) ) ;
#13400=CARTESIAN_POINT ( 'NONE',  ( -33.02621722254092873, 8.688004171162605260, 16.87568207617864502 ) ) ;
#13401=DIRECTION ( 'NONE',  ( 0.000000000000000000, -2.185478394931410082E-16, 1.000000000000000000 ) ) ;
#13403=CARTESIAN_POINT ( 'NONE',  ( -19.99969986081099904, -13.50737899243800122, 61.71206422150099513 ) ) ;
#13407=VERTEX_POINT ( 'NONE', #11910 ) ;
#13410=CARTESIAN_POINT ( 'NONE',  ( 0.8003001391889992266, 11.99262100756199878, 16.16206422150100153 ) ) ;
#13421=DIRECTION ( 'NONE',  ( 0.000000000000000000, -1.000000000000000000, -1.224646799147350002E-16 ) ) ;
#13427=CLOSED_SHELL ( 'NONE', ( #2799, #10318, #6421, #14962, #8310, #13952, #9281, #12246, #5689, #14854, #10305, #14213, #3467, #13727, #2163, #14686, #8473, #14506, #12916, #1932, #13641, #4350, #4304, #13563, #11412, #12005, #12294, #3194, #3378, #11292, #5130, #8574, #3495, #12697, #14749, #14314, #6902, #10418, #14127, #1052, #4494, #4818, #12934, #9050, #14984, #1100, #5518, #5043, #1191, #6129, #7483, #2889, #12118, #140, #7561, #2947, #3935, #2742, #9243, #2647, #2651, #6112, #6173, #7659, #6508, #4006, #1784, #2067, #5686, #10811, #14002, #939, #9558, #779, #5619, #11340, #899, #14286, #8866, #7379, #12857 ) ) ;
#13433=DIRECTION ( 'NONE',  ( 1.000000000000000000, -1.499759782661860071E-32, 1.224646799147350002E-16 ) ) ;
#13443=CONICAL_SURFACE ( 'NONE', #10250, 6.250000000000001776, 0.7853981633974461696 ) ;
#13453=EDGE_LOOP ( 'NONE', ( #1694, #8634 ) ) ;
#13464=CARTESIAN_POINT ( 'NONE',  ( -33.37394235882850069, 7.183219930803497633, 17.76912582958182085 ) ) ;
#13467=ORIENTED_EDGE ( 'NONE', *, *, #11357, .F. ) ;
#13468=EDGE_CURVE ( 'NONE', #4184, #7451, #6230, .T. ) ;
#13469=VERTEX_POINT ( 'NONE', #4955 ) ;
#13478=CYLINDRICAL_SURFACE ( 'NONE', #2622, 19.00000000000000000 ) ;
#13484=VERTEX_POINT ( 'NONE', #5170 ) ;
#13488=ORIENTED_EDGE ( 'NONE', *, *, #3047, .T. ) ;
#13490=CARTESIAN_POINT ( 'NONE',  ( -14.33378105012738502, -9.151149813406526334, -13.27091190697294998 ) ) ;
#13509=CARTESIAN_POINT ( 'NONE',  ( 3.680924773572380904, 6.563493760827302737, 18.28413564240387856 ) ) ;
#13510=CARTESIAN_POINT ( 'NONE',  ( 4.185908152460800835, 11.99262100756689620, 32.26206422150099939 ) ) ;
#13512=DIRECTION ( 'NONE',  ( 0.000000000000000000, -1.000000000000000000, -1.224646799147350002E-16 ) ) ;
#13514=VERTEX_POINT ( 'NONE', #587 ) ;
#13515=DIRECTION ( 'NONE',  ( 0.000000000000000000, -2.220446049250313081E-16, 1.000000000000000000 ) ) ;
#13517=ORIENTED_EDGE ( 'NONE', *, *, #6887, .T. ) ;
#13520=CIRCLE ( 'NONE', #10341, 37.50000000000000000 ) ;
#13528=FACE_OUTER_BOUND ( 'NONE', #12970, .T. ) ;
#13529=AXIS2_PLACEMENT_3D ( 'NONE', #2829, #7485, #6780 ) ;
#13530=DIRECTION ( 'NONE',  ( 0.000000000000000000, 1.131341397376178572E-16, -1.000000000000000000 ) ) ;
#13548=VECTOR ( 'NONE', #9020, 1000.000000000000000 ) ;
#13550=VECTOR ( 'NONE', #12768, 1000.000000000000000 ) ;
#13556=CARTESIAN_POINT ( 'NONE',  ( 16.19611543458935898, -30.09219076442761676, 44.25382773196126607 ) ) ;
#13563=ADVANCED_FACE ( 'NONE', ( #14732 ), #6456, .T. ) ;
#13564=CARTESIAN_POINT ( 'NONE',  ( 2.234407040561845026, 7.699995122702122607, 17.38035637616411222 ) ) ;
#13566=CARTESIAN_POINT ( 'NONE',  ( -15.49969986081099904, 71.39262100756199914, 24.21206422150100579 ) ) ;
#13570=CARTESIAN_POINT ( 'NONE',  ( 0.8003001391889992266, 11.99262100756199878, 24.16206422150099442 ) ) ;
#13574=ORIENTED_EDGE ( 'NONE', *, *, #8016, .F. ) ;
#13579=ORIENTED_EDGE ( 'NONE', *, *, #2040, .F. ) ;
#13580=DIRECTION ( 'NONE',  ( 0.000000000000000000, -1.225619847157526848E-16, 1.000000000000000000 ) ) ;
#13593=CARTESIAN_POINT ( 'NONE',  ( -7.499699860810999041, -19.50737899243799589, 6.712064221500998684 ) ) ;
#13596=CARTESIAN_POINT ( 'NONE',  ( 2.026817500918900006, 8.688004171162612366, 31.54844636682341275 ) ) ;
#13598=AXIS2_PLACEMENT_3D ( 'NONE', #10929, #9707, #233 ) ;
#13609=CARTESIAN_POINT ( 'NONE',  ( -32.98605307870397496, 8.906201437969643919, 31.64365951543691935 ) ) ;
#13622=CARTESIAN_POINT ( 'NONE',  ( 0.8003001391889992266, 11.99262100756199878, 24.26206422150100295 ) ) ;
#13623=AXIS2_PLACEMENT_3D ( 'NONE', #3425, #4354, #1204 ) ;
#13628=CARTESIAN_POINT ( 'NONE',  ( 16.90549927255504059, -30.26092226866779100, 43.08547782963380968 ) ) ;
#13629=ORIENTED_EDGE ( 'NONE', *, *, #15020, .T. ) ;
#13631=ORIENTED_EDGE ( 'NONE', *, *, #3453, .T. ) ;
#13635=CARTESIAN_POINT ( 'NONE',  ( -10.99969986081100082, -13.50737899243800122, 61.71206422150099513 ) ) ;
#13637=CIRCLE ( 'NONE', #7015, 37.50000000000000000 ) ;
#13641=ADVANCED_FACE ( 'NONE', ( #9132 ), #7055, .F. ) ;
#13643=DIRECTION ( 'NONE',  ( 0.000000000000000000, -1.000000000000000000, -1.224646799147350002E-16 ) ) ;
#13656=AXIS2_PLACEMENT_3D ( 'NONE', #2255, #6900, #5536 ) ;
#13658=CARTESIAN_POINT ( 'NONE',  ( 1.760741030006599317, 10.68321993080349763, 16.26994987741148790 ) ) ;
#13662=EDGE_CURVE ( 'NONE', #12839, #10153, #9286, .T. ) ;
#13664=CARTESIAN_POINT ( 'NONE',  ( 5.324488449731577866, 5.776599650193906754, 29.29976833248339574 ) ) ;
#13668=FACE_OUTER_BOUND ( 'NONE', #3582, .T. ) ;
#13676=CARTESIAN_POINT ( 'NONE',  ( -15.49969986081099904, 22.99262100756200056, 24.21206422150099868 ) ) ;
#13698=CYLINDRICAL_SURFACE ( 'NONE', #8457, 3.249999999999999556 ) ;
#13709=ORIENTED_EDGE ( 'NONE', *, *, #8537, .T. ) ;
#13718=CARTESIAN_POINT ( 'NONE',  ( 18.52080869893816839, -26.54306194185273426, 39.98729300097398465 ) ) ;
#13727=ADVANCED_FACE ( 'NONE', ( #11435 ), #339, .F. ) ;
#13733=CARTESIAN_POINT ( 'NONE',  ( 15.21039067757261520, -24.94558503991284226, 2.690838063943358449 ) ) ;
#13734=CARTESIAN_POINT ( 'NONE',  ( -15.49969986081099904, 20.99262100756200056, 32.26206422150099939 ) ) ;
#13739=DIRECTION ( 'NONE',  ( -1.000000000000000000, 1.499759782661860071E-32, -1.224646799147350002E-16 ) ) ;
#13741=CARTESIAN_POINT ( 'NONE',  ( 22.00030013918900096, -27.00737899243800300, 5.212064221501000461 ) ) ;
#13748=CIRCLE ( 'NONE', #13030, 5.250000000000000888 ) ;
#13755=LINE ( 'NONE', #7552, #9638 ) ;
#13756=ORIENTED_EDGE ( 'NONE', *, *, #1220, .F. ) ;
#13770=DIRECTION ( 'NONE',  ( 0.000000000000000000, 9.130123557772668334E-17, -1.000000000000000000 ) ) ;
#13778=VECTOR ( 'NONE', #4430, 1000.000000000000000 ) ;
#13781=CARTESIAN_POINT ( 'NONE',  ( 18.44249865551014622, -28.13424414313808697, 40.15532763027508167 ) ) ;
#13794=EDGE_CURVE ( 'NONE', #3050, #3447, #8790, .T. ) ;
#13797=CARTESIAN_POINT ( 'NONE',  ( 15.62447441151310557, -24.37627644466446952, 45.13040448977423580 ) ) ;
#13800=ORIENTED_EDGE ( 'NONE', *, *, #8124, .F. ) ;
#13802=CARTESIAN_POINT ( 'NONE',  ( 7.200737182676100190, 4.873818854045000037, 20.51204286552489009 ) ) ;
#13815=CARTESIAN_POINT ( 'NONE',  ( -15.49969986081099904, 4.873818854045000037, 24.21206422150099868 ) ) ;
#13818=CARTESIAN_POINT ( 'NONE',  ( 4.185908152463202470, 11.99262100756819827, 16.16206422150100153 ) ) ;
#13823=DIRECTION ( 'NONE',  ( 0.000000000000000000, 1.000000000000000000, 1.224646799147350002E-16 ) ) ;
#13828=CARTESIAN_POINT ( 'NONE',  ( -32.76014075162859740, 10.68321993080349763, 32.15417856559049881 ) ) ;
#13837=ORIENTED_EDGE ( 'NONE', *, *, #7592, .T. ) ;
#13844=CARTESIAN_POINT ( 'NONE',  ( -5.831322665684755435, -10.89379466358441384, 60.44451731831637886 ) ) ;
#13846=CARTESIAN_POINT ( 'NONE',  ( 0.8003001391889992266, 3.992621007561997892, 24.21206422150099868 ) ) ;
#13851=ORIENTED_EDGE ( 'NONE', *, *, #558, .T. ) ;
#13852=CARTESIAN_POINT ( 'NONE',  ( 17.35529208743007601, -30.13086992362137551, 42.29099036764831965 ) ) ;
#13855=CARTESIAN_POINT ( 'NONE',  ( -21.60465186766506918, -5.558554322211025855, 61.21584607775863418 ) ) ;
#13865=AXIS2_PLACEMENT_3D ( 'NONE', #287, #8459, #9909 ) ;
#13870=CARTESIAN_POINT ( 'NONE',  ( 14.70449519813618977, -26.54667573212512011, 46.43727775870232222 ) ) ;
#13875=FACE_OUTER_BOUND ( 'NONE', #6739, .T. ) ;
#13879=VECTOR ( 'NONE', #4363, 1000.000000000000000 ) ;
#13888=CARTESIAN_POINT ( 'NONE',  ( 5.491220283057865359, 5.696595093589351677, 29.19866481050043561 ) ) ;
#13890=DIRECTION ( 'NONE',  ( 0.000000000000000000, 9.130123557772668334E-17, -1.000000000000000000 ) ) ;
#13891=CARTESIAN_POINT ( 'NONE',  ( -19.85590761163705409, -14.67339121653544964, -13.03410041670467301 ) ) ;
#13899=AXIS2_PLACEMENT_3D ( 'NONE', #13570, #4005, #6359 ) ;
#13906=CARTESIAN_POINT ( 'NONE',  ( -15.49969986081099904, -2.007378992438000331, 24.21206422150099513 ) ) ;
#13909=CARTESIAN_POINT ( 'NONE',  ( -34.68032449512179483, 6.563493760861876858, 30.13999280063012520 ) ) ;
#13915=DIRECTION ( 'NONE',  ( 0.000000000000000000, 1.224646799147350002E-16, -1.000000000000000000 ) ) ;
#13918=AXIS2_PLACEMENT_3D ( 'NONE', #13381, #4042, #12148 ) ;
#13920=DIRECTION ( 'NONE',  ( 0.000000000000000000, 1.131341397376178572E-16, -1.000000000000000000 ) ) ;
#13924=DIRECTION ( 'NONE',  ( -1.000000000000000000, 0.000000000000000000, 0.000000000000000000 ) ) ;
#13931=CARTESIAN_POINT ( 'NONE',  ( -20.79173795306330774, -5.016115743661099913, 61.33778859824581531 ) ) ;
#13932=ORIENTED_EDGE ( 'NONE', *, *, #2230, .T. ) ;
#13939=EDGE_CURVE ( 'NONE', #12240, #1569, #3436, .T. ) ;
#13943=CARTESIAN_POINT ( 'NONE',  ( -14.33039451911155382, -17.86275798826623173, -13.27081260207403268 ) ) ;
#13948=FACE_OUTER_BOUND ( 'NONE', #2607, .T. ) ;
#13950=ORIENTED_EDGE ( 'NONE', *, *, #4702, .T. ) ;
#13952=ADVANCED_FACE ( 'NONE', ( #4588 ), #543, .T. ) ;
#13954=CARTESIAN_POINT ( 'NONE',  ( 3.243537350856608548, 11.48902252479464181, 16.16206422150199629 ) ) ;
#13957=CARTESIAN_POINT ( 'NONE',  ( -15.49969986081099904, 10.68321993080349586, 43.21206422150100224 ) ) ;
#13958=DIRECTION ( 'NONE',  ( 0.000000000000000000, 0.000000000000000000, 1.000000000000000000 ) ) ;
#13960=FACE_OUTER_BOUND ( 'NONE', #1282, .T. ) ;
#13962=ORIENTED_EDGE ( 'NONE', *, *, #3666, .F. ) ;
#13970=DIRECTION ( 'NONE',  ( 0.000000000000000000, -9.130123557772668334E-17, 1.000000000000000000 ) ) ;
#13977=CARTESIAN_POINT ( 'NONE',  ( -34.24293707247814211, 11.48902252479439134, 32.26206422149999753 ) ) ;
#13981=AXIS2_PLACEMENT_3D ( 'NONE', #2868, #9973, #3738 ) ;
#13988=CARTESIAN_POINT ( 'NONE',  ( -15.49969986081099904, -19.50737899243800300, 24.21206422150100224 ) ) ;
#13994=DIRECTION ( 'NONE',  ( 0.000000000000000000, -1.000000000000000000, -1.224646799147350002E-16 ) ) ;
#14001=CARTESIAN_POINT ( 'NONE',  ( -31.13003983167857669, -27.07585217469821259, 58.39162460182396330 ) ) ;
#14002=ADVANCED_FACE ( 'NONE', ( #994 ), #5570, .T. ) ;
#14006=CARTESIAN_POINT ( 'NONE',  ( -16.15343032139029233, -3.507358680200116208, 61.71206438550458984 ) ) ;
#14011=CARTESIAN_POINT ( 'NONE',  ( -15.49969986081099904, 0.9926210075619987805, 24.21206422150099868 ) ) ;
#14018=AXIS2_PLACEMENT_3D ( 'NONE', #10538, #8469, #71 ) ;
#14028=ORIENTED_EDGE ( 'NONE', *, *, #980, .F. ) ;
#14029=LINE ( 'NONE', #3546, #6152 ) ;
#14037=DIRECTION ( 'NONE',  ( -1.000000000000000000, 0.000000000000000000, 0.000000000000000000 ) ) ;
#14039=CIRCLE ( 'NONE', #6453, 15.62500000000000355 ) ;
#14040=DIRECTION ( 'NONE',  ( 0.000000000000000000, 0.4999999999999993339, 0.8660254037844390407 ) ) ;
#14060=EDGE_LOOP ( 'NONE', ( #1397, #6208, #6145, #2246, #9048, #9735, #12926 ) ) ;
#14061=CARTESIAN_POINT ( 'NONE',  ( -15.49969986081099904, 71.39262100756199914, 24.21206422150100579 ) ) ;
#14070=CARTESIAN_POINT ( 'NONE',  ( -7.499699860810999041, -19.50737899243799589, 60.84879442494580104 ) ) ;
#14072=CIRCLE ( 'NONE', #7468, 19.00000000000000000 ) ;
#14080=CARTESIAN_POINT ( 'NONE',  ( 13.85920135429429934, -27.00737899243800300, 5.212064221501000461 ) ) ;
#14092=AXIS2_PLACEMENT_3D ( 'NONE', #9018, #5650, #2145 ) ;
#14097=CARTESIAN_POINT ( 'NONE',  ( -12.75469031341037685, -17.08519519190822322, -13.18812972638144743 ) ) ;
#14099=EDGE_LOOP ( 'NONE', ( #1624, #1978, #1885, #4601 ) ) ;
#14100=CIRCLE ( 'NONE', #8717, 2.500000000000000444 ) ;
#14101=EDGE_LOOP ( 'NONE', ( #1641, #3841, #5003, #12180, #14426, #14816, #7877, #9371, #9177, #9714, #1677, #143, #2564, #12523, #5918, #14134, #13323, #8197, #5616, #7219, #4986, #8449, #5999 ) ) ;
#14112=CARTESIAN_POINT ( 'NONE',  ( -37.04494295528539993, 12.99262100756199878, 32.26206422150099939 ) ) ;
#14114=B_SPLINE_CURVE_WITH_KNOTS ( 'NONE', 3,
 ( #138, #9452, #14126, #209, #6155, #367, #3649, #9685 ),
 .UNSPECIFIED., .F., .F.,
 ( 4, 2, 2, 4 ),
 ( 0.000000000000000000, 0.2500000000000007216, 0.5000000000000014433, 1.000000000000000000 ),
 .UNSPECIFIED. ) ;
#14120=CARTESIAN_POINT ( 'NONE',  ( 21.94825106416211824, -29.59105673714036300, 22.22908312652625540 ) ) ;
#14121=AXIS2_PLACEMENT_3D ( 'NONE', #14011, #12870, #9260 ) ;
#14125=EDGE_CURVE ( 'NONE', #10705, #12498, #6413, .T. ) ;
#14126=CARTESIAN_POINT ( 'NONE',  ( 7.492258075141476681, 4.011311318234621837, 24.89656457396599265 ) ) ;
#14127=ADVANCED_FACE ( 'NONE', ( #1445, #5948 ), #7168, .F. ) ;
#14134=ORIENTED_EDGE ( 'NONE', *, *, #7206, .F. ) ;
#14136=CARTESIAN_POINT ( 'NONE',  ( -35.89253646483789595, 5.983413651708109349, 29.54306818915388533 ) ) ;
#14141=AXIS2_PLACEMENT_3D ( 'NONE', #1888, #6534, #2954 ) ;
#14148=EDGE_CURVE ( 'NONE', #700, #9278, #794, .T. ) ;
#14152=CARTESIAN_POINT ( 'NONE',  ( 18.17353442779068473, -29.10076824620873026, 7.707990019632498857 ) ) ;
#14159=UNCERTAINTY_MEASURE_WITH_UNIT (LENGTH_MEASURE( 1.000000000000000082E-05 ), #9265, 'distance_accuracy_value', 'NONE');
#14162=CARTESIAN_POINT ( 'NONE',  ( 0.8003001391889992266, 20.99262100756200056, 24.21206422150099868 ) ) ;
#14169=CARTESIAN_POINT ( 'NONE',  ( 4.185908152460800835, 11.99262100756689620, 32.26206422150099939 ) ) ;
#14172=CARTESIAN_POINT ( 'NONE',  ( -19.07412756035248336, -10.75766711226809669, -13.11755961025760442 ) ) ;
#14174=DIRECTION ( 'NONE',  ( -1.000000000000000000, -1.927249326158839857E-15, 7.070501591499359300E-17 ) ) ;
#14178=ORIENTED_EDGE ( 'NONE', *, *, #4551, .F. ) ;
#14183=DIRECTION ( 'NONE',  ( 0.000000000000000000, 1.131341397376178572E-16, -1.000000000000000000 ) ) ;
#14185=CARTESIAN_POINT ( 'NONE',  ( -15.49969986081099904, 64.39262100756199914, 24.21206422150100224 ) ) ;
#14187=DIRECTION ( 'NONE',  ( 0.000000000000000000, -1.000000000000000000, -1.224646799147350002E-16 ) ) ;
#14189=DIRECTION ( 'NONE',  ( 0.000000000000000000, 1.508455196501571429E-16, -1.000000000000000000 ) ) ;
#14196=EDGE_CURVE ( 'NONE', #8556, #4184, #4951, .T. ) ;
#14200=EDGE_CURVE ( 'NONE', #2938, #10535, #14377, .T. ) ;
#14213=ADVANCED_FACE ( 'NONE', ( #10141 ), #10311, .T. ) ;
#14214=DIRECTION ( 'NONE',  ( 0.000000000000000000, -1.225619847157526848E-16, 1.000000000000000000 ) ) ;
#14216=CARTESIAN_POINT ( 'NONE',  ( 0.8003001391889992266, 3.992621007561997892, 24.16206422150099442 ) ) ;
#14224=EDGE_CURVE ( 'NONE', #12498, #13305, #5183, .T. ) ;
#14257=VERTEX_POINT ( 'NONE', #12302 ) ;
#14261=FACE_OUTER_BOUND ( 'NONE', #4924, .T. ) ;
#14266=EDGE_CURVE ( 'NONE', #3050, #9211, #5485, .T. ) ;
#14269=CARTESIAN_POINT ( 'NONE',  ( -38.24611845019376943, 4.729174316169127756, 27.62997877663899615 ) ) ;
#14270=EDGE_LOOP ( 'NONE', ( #10367, #3939, #2001, #10732 ) ) ;
#14277=ORIENTED_EDGE ( 'NONE', *, *, #8077, .F. ) ;
#14286=ADVANCED_FACE ( 'NONE', ( #13528 ), #6543, .F. ) ;
#14289=DIRECTION ( 'NONE',  ( 0.000000000000000000, 0.000000000000000000, 1.000000000000000000 ) ) ;
#14293=ORIENTED_EDGE ( 'NONE', *, *, #9823, .T. ) ;
#14295=ORIENTED_EDGE ( 'NONE', *, *, #3666, .T. ) ;
#14304=EDGE_CURVE ( 'NONE', #9332, #3162, #14594, .T. ) ;
#14305=ORIENTED_EDGE ( 'NONE', *, *, #6434, .F. ) ;
#14308=CARTESIAN_POINT ( 'NONE',  ( -15.49969986081099904, 22.99262100756200411, 8.587064221501004013 ) ) ;
#14309=ORIENTED_EDGE ( 'NONE', *, *, #7452, .F. ) ;
#14313=VERTEX_POINT ( 'NONE', #10999 ) ;
#14314=ADVANCED_FACE ( 'NONE', ( #7546 ), #7621, .T. ) ;
#14324=CARTESIAN_POINT ( 'NONE',  ( -16.95049030215496089, -9.237476495170920288, -13.26085252337267484 ) ) ;
#14326=ORIENTED_EDGE ( 'NONE', *, *, #5698, .F. ) ;
#14327=DIRECTION ( 'NONE',  ( 0.000000000000000000, -1.000000000000000000, -1.224646799147350002E-16 ) ) ;
#14330=FACE_OUTER_BOUND ( 'NONE', #3731, .T. ) ;
#14337=CYLINDRICAL_SURFACE ( 'NONE', #79, 3.249999999999999556 ) ;
#14339=FACE_BOUND ( 'NONE', #7560, .T. ) ;
#14343=DIRECTION ( 'NONE',  ( 0.000000000000000000, 1.000000000000000000, 1.224646799147350002E-16 ) ) ;
#14347=DIRECTION ( 'NONE',  ( 0.000000000000000000, 0.000000000000000000, 1.000000000000000000 ) ) ;
#14348=ORIENTED_EDGE ( 'NONE', *, *, #10669, .T. ) ;
#14349=ORIENTED_EDGE ( 'NONE', *, *, #13939, .T. ) ;
#14350=CARTESIAN_POINT ( 'NONE',  ( 22.00028543145668536, -30.25720928778257246, 23.99491965613809086 ) ) ;
#14354=LINE ( 'NONE', #1780, #14761 ) ;
#14356=EDGE_CURVE ( 'NONE', #11202, #10535, #11231, .T. ) ;
#14362=DIRECTION ( 'NONE',  ( 3.632077277826439854E-16, -1.000000000000000000, 0.000000000000000000 ) ) ;
#14370=VERTEX_POINT ( 'NONE', #12607 ) ;
#14376=VECTOR ( 'NONE', #8793, 1000.000000000000000 ) ;
#14377=LINE ( 'NONE', #3891, #12038 ) ;
#14379=CARTESIAN_POINT ( 'NONE',  ( 18.44182102609496354, -28.13808047628806719, 8.267357603750861372 ) ) ;
#14381=VERTEX_POINT ( 'NONE', #12840 ) ;
#14389=ORIENTED_EDGE ( 'NONE', *, *, #333, .T. ) ;
#14395=CARTESIAN_POINT ( 'NONE',  ( -12.27197285165629737, -4.041276922754793333, 61.57424106746455550 ) ) ;
#14401=CARTESIAN_POINT ( 'NONE',  ( -15.49969986081099904, 4.873818854045002702, 1.212064221501000461 ) ) ;
#14402=ORIENTED_EDGE ( 'NONE', *, *, #8789, .T. ) ;
#14408=EDGE_CURVE ( 'NONE', #11422, #8216, #7921, .T. ) ;
#14412=DIRECTION ( 'NONE',  ( 0.000000000000000000, 0.000000000000000000, 1.000000000000000000 ) ) ;
#14416=CARTESIAN_POINT ( 'NONE',  ( -38.20013690429809827, 4.873818854045000037, 20.51204286552489009 ) ) ;
#14421=VERTEX_POINT ( 'NONE', #11451 ) ;
#14423=CARTESIAN_POINT ( 'NONE',  ( 21.86100802344563832, -27.43036982981187677, 20.98262938449914117 ) ) ;
#14426=ORIENTED_EDGE ( 'NONE', *, *, #2403, .T. ) ;
#14437=CARTESIAN_POINT ( 'NONE',  ( 21.86816044869649289, -26.16306096081211052, 21.06647100910851123 ) ) ;
#14438=DIRECTION ( 'NONE',  ( 0.000000000000000000, -1.000000000000000000, -1.224646799147350002E-16 ) ) ;
#14440=CARTESIAN_POINT ( 'NONE',  ( -28.78282149594069850, -31.14135358865360104, 59.28069236156870403 ) ) ;
#14445=DIRECTION ( 'NONE',  ( 0.000000000000000000, 0.000000000000000000, -1.000000000000000000 ) ) ;
#14447=CARTESIAN_POINT ( 'NONE',  ( 17.02627693417459298, -30.24626016961038744, 5.547585651947908758 ) ) ;
#14454=ORIENTED_EDGE ( 'NONE', *, *, #4988, .T. ) ;
#14463=VECTOR ( 'NONE', #7501, 1000.000000000000000 ) ;
#14465=CARTESIAN_POINT ( 'NONE',  ( 13.85920135429429934, -27.00737899243800300, 7.712064221501001349 ) ) ;
#14493=CARTESIAN_POINT ( 'NONE',  ( -15.49969986081099904, 37.56536188261469533, 18.96206422150100224 ) ) ;
#14500=AXIS2_PLACEMENT_3D ( 'NONE', #1567, #5092, #4790 ) ;
#14501=CARTESIAN_POINT ( 'NONE',  ( 0.8003001391889992266, 11.99262100756199878, 32.26206422150099939 ) ) ;
#14506=ADVANCED_FACE ( 'NONE', ( #1428 ), #1692, .F. ) ;
#14507=B_SPLINE_CURVE_WITH_KNOTS ( 'NONE', 3,
 ( #7173, #6179, #12008, #8632, #14379, #7476, #460, #14152, #7326, #12151, #3895, #4902, #5047, #3745, #1450, #14447, #8554, #13015, #10861, #7404, #6326, #1527, #5190, #10782, #13165, #2597, #9783, #13316, #3972, #8323, #11852, #12085, #13239, #3672 ),
 .UNSPECIFIED., .F., .F.,
 ( 4, 2, 2, 2, 2, 2, 2, 2, 2, 2, 2, 2, 2, 2, 2, 2, 4 ),
 ( 0.000000000000000000, 0.0006891453135227206461, 0.001378290627045441292, 0.002067435940568161830, 0.002756581254090882584, 0.003445726567613603773, 0.004134871881136323660, 0.004824017194659043981, 0.005513162508181765169, 0.006202307821704486357, 0.006891453135227207545, 0.007580598448749926131, 0.008269743762272647319, 0.008958889075795369375, 0.009648034389318091431, 0.01033717970284081349, 0.01102632501636353554 ),
 .UNSPECIFIED. ) ;
#14508=DIRECTION ( 'NONE',  ( 0.000000000000000000, 1.000000000000000000, 1.224646799147350002E-16 ) ) ;
#14516=CARTESIAN_POINT ( 'NONE',  ( 21.87338300223960985, -25.95928379819316234, 27.29579227643073835 ) ) ;
#14527=DIRECTION ( 'NONE',  ( 0.000000000000000000, 1.000000000000000000, 1.224646799147350002E-16 ) ) ;
#14532=VERTEX_POINT ( 'NONE', #7147 ) ;
#14542=CARTESIAN_POINT ( 'NONE',  ( -33.23672817421918779, 7.708027139131385930, 17.39831465307906555 ) ) ;
#14546=FACE_OUTER_BOUND ( 'NONE', #5793, .T. ) ;
#14549=CARTESIAN_POINT ( 'NONE',  ( -7.499699860810999041, -19.50737899243799589, 6.712064221500998684 ) ) ;
#14560=CARTESIAN_POINT ( 'NONE',  ( -15.49969986081099371, -2.007378992437995890, -13.28793577849899243 ) ) ;
#14563=CARTESIAN_POINT ( 'NONE',  ( -34.68296123826191035, 6.562241739503763327, 18.28527686625572457 ) ) ;
#14566=EDGE_LOOP ( 'NONE', ( #2100, #8763, #3442, #11031, #13756, #10827, #12407, #5258, #10962 ) ) ;
#14567=CARTESIAN_POINT ( 'NONE',  ( -2.216578225681298697, -32.00737899243799944, -11.04189727591769632 ) ) ;
#14570=CARTESIAN_POINT ( 'NONE',  ( 21.87337189122190040, -28.05484980333040923, 21.12821865650454711 ) ) ;
#14571=CARTESIAN_POINT ( 'NONE',  ( 0.8003001391889992266, 20.99262100756200056, 32.26206422150099939 ) ) ;
#14573=PLANE ( 'NONE',  #13981 ) ;
#14575=EDGE_CURVE ( 'NONE', #11915, #11355, #2427, .T. ) ;
#14577=CARTESIAN_POINT ( 'NONE',  ( 6.045543233663400073, 12.99262100756199878, 32.26206422150099939 ) ) ;
#14585=DIRECTION ( 'NONE',  ( -1.000000000000000000, 0.000000000000000000, 0.000000000000000000 ) ) ;
#14587=CARTESIAN_POINT ( 'NONE',  ( 21.87335010765016108, -25.96044300975462349, 21.12793889599969077 ) ) ;
#14594=LINE ( 'NONE', #11229, #493 ) ;
#14601=CARTESIAN_POINT ( 'NONE',  ( -32.81697519099675020, 10.05207975130290521, 32.03010237117641168 ) ) ;
#14614=CARTESIAN_POINT ( 'NONE',  ( -15.49969986081099904, 70.81438635534659909, 24.21206422150100579 ) ) ;
#14617=DIRECTION ( 'NONE',  ( 0.000000000000000000, 9.130123557772668334E-17, -1.000000000000000000 ) ) ;
#14634=AXIS2_PLACEMENT_3D ( 'NONE', #13988, #1128, #2132 ) ;
#14636=EDGE_CURVE ( 'NONE', #12333, #4377, #14114, .T. ) ;
#14638=CARTESIAN_POINT ( 'NONE',  ( -35.52696516869671228, 6.159096188266306449, 18.68424166250937901 ) ) ;
#14640=PLANE ( 'NONE',  #2641 ) ;
#14643=CARTESIAN_POINT ( 'NONE',  ( 13.85920135429429934, -27.00737899243800300, 5.212064221501000461 ) ) ;
#14647=VERTEX_POINT ( 'NONE', #4094 ) ;
#14651=CARTESIAN_POINT ( 'NONE',  ( 4.904576926706878837, 5.977929128642318624, 18.88727191237769887 ) ) ;
#14654=CARTESIAN_POINT ( 'NONE',  ( 16.55265521278991869, -23.76699243818182339, 4.741285470919336831 ) ) ;
#14663=EDGE_CURVE ( 'NONE', #4618, #8805, #10661, .T. ) ;
#14664=CIRCLE ( 'NONE', #2202, 37.50000000000000000 ) ;
#14668=DIRECTION ( 'NONE',  ( 0.000000000000000000, 0.000000000000000000, 1.000000000000000000 ) ) ;
#14677=DIRECTION ( 'NONE',  ( 1.000000000000000000, 3.700743415417188632E-16, 0.000000000000000000 ) ) ;
#14683=ORIENTED_EDGE ( 'NONE', *, *, #7054, .F. ) ;
#14686=ADVANCED_FACE ( 'NONE', ( #1648 ), #13443, .F. ) ;
#14694=CARTESIAN_POINT ( 'NONE',  ( 17.24684023006172140, -30.18180943203350708, 42.48680623383349797 ) ) ;
#14697=CARTESIAN_POINT ( 'NONE',  ( -15.49968909271368211, -3.507379016232285096, 61.71092834827113194 ) ) ;
#14702=CARTESIAN_POINT ( 'NONE',  ( 1.947694826113897770, 9.133458655267698845, 16.68946746569451278 ) ) ;
#14712=AXIS2_PLACEMENT_3D ( 'NONE', #6632, #3289, #9012 ) ;
#14716=LINE ( 'NONE', #566, #2476 ) ;
#14722=DIRECTION ( 'NONE',  ( 0.000000000000000000, -1.000000000000000000, -1.224646799147350002E-16 ) ) ;
#14726=EDGE_CURVE ( 'NONE', #609, #12884, #12211, .T. ) ;
#14730=DIRECTION ( 'NONE',  ( -7.070501591499390115E-17, 1.224646799147350002E-16, -1.000000000000000000 ) ) ;
#14732=FACE_OUTER_BOUND ( 'NONE', #11643, .T. ) ;
#14734=ORIENTED_EDGE ( 'NONE', *, *, #10394, .F. ) ;
#14743=EDGE_LOOP ( 'NONE', ( #12728, #3483, #930, #11082, #1812 ) ) ;
#14749=ADVANCED_FACE ( 'NONE', ( #6373 ), #11060, .F. ) ;
#14753=APPLICATION_CONTEXT ( 'automotive_design' ) ;
#14754=ORIENTED_EDGE ( 'NONE', *, *, #1117, .F. ) ;
#14757=ORIENTED_EDGE ( 'NONE', *, *, #9640, .F. ) ;
#14758=CARTESIAN_POINT ( 'NONE',  ( -31.79969986081099975, 11.99262100756199878, 32.26206422150099939 ) ) ;
#14761=VECTOR ( 'NONE', #11718, 1000.000000000000000 ) ;
#14769=EDGE_CURVE ( 'NONE', #10220, #6353, #3169, .T. ) ;
#14770=CARTESIAN_POINT ( 'NONE',  ( -7.561698276841002375, -7.413715827245769496, 60.86289348305165703 ) ) ;
#14775=CARTESIAN_POINT ( 'NONE',  ( -15.49969986081099904, -2.007378992438000331, 24.21206422150099513 ) ) ;
#14784=EDGE_CURVE ( 'NONE', #10153, #5382, #7900, .T. ) ;
#14790=CARTESIAN_POINT ( 'NONE',  ( 17.25200030867059553, -23.81382647575409806, 42.48144389911218610 ) ) ;
#14803=LINE ( 'NONE', #12438, #1561 ) ;
#14816=ORIENTED_EDGE ( 'NONE', *, *, #4070, .T. ) ;
#14830=DIRECTION ( 'NONE',  ( 0.000000000000000000, 0.000000000000000000, 1.000000000000000000 ) ) ;
#14834=LINE ( 'NONE', #10241, #13879 ) ;
#14835=CONICAL_SURFACE ( 'NONE', #1645, 1664.279482350500075, 1.029744258676650093 ) ;
#14843=CARTESIAN_POINT ( 'NONE',  ( -38.44424205229172031, 4.142642748859736379, 22.58640670738479983 ) ) ;
#14847=ORIENTED_EDGE ( 'NONE', *, *, #9440, .F. ) ;
#14848=CARTESIAN_POINT ( 'NONE',  ( 15.84747201894258772, -29.85305842324876835, 44.79472527846461816 ) ) ;
#14851=CARTESIAN_POINT ( 'NONE',  ( -22.79913995068414678, -6.663256836605895295, 60.99553151634774650 ) ) ;
#14852=ORIENTED_EDGE ( 'NONE', *, *, #5698, .T. ) ;
#14854=ADVANCED_FACE ( 'NONE', ( #8052 ), #14898, .T. ) ;
#14865=ORIENTED_EDGE ( 'NONE', *, *, #6700, .F. ) ;
#14866=CARTESIAN_POINT ( 'NONE',  ( 18.29963344931381286, -25.27049385225708278, 40.45631929470508936 ) ) ;
#14879=LINE ( 'NONE', #14949, #9242 ) ;
#14880=LINE ( 'NONE', #5466, #11927 ) ;
#14882=DIRECTION ( 'NONE',  ( 0.000000000000000000, -1.334178587669858246E-16, 1.000000000000000000 ) ) ;
#14883=CARTESIAN_POINT ( 'NONE',  ( 6.590007710802169072, 5.168430268676311279, 28.44896274323930285 ) ) ;
#14886=EDGE_CURVE ( 'NONE', #1644, #1569, #14879, .T. ) ;
#14895=ORIENTED_EDGE ( 'NONE', *, *, #6607, .F. ) ;
#14898=CONICAL_SURFACE ( 'NONE', #13656, 19.00000000000000000, 1.047197551196598297 ) ;
#14903=AXIS2_PLACEMENT_3D ( 'NONE', #8130, #12821, #6829 ) ;
#14905=FACE_OUTER_BOUND ( 'NONE', #10842, .T. ) ;
#14909=CARTESIAN_POINT ( 'NONE',  ( -15.49969986081099904, 37.56536188261469533, 29.46206422150100579 ) ) ;
#14922=DIRECTION ( 'NONE',  ( 0.000000000000000000, 1.239088197126290817E-16, -1.000000000000000000 ) ) ;
#14923=ORIENTED_EDGE ( 'NONE', *, *, #9513, .T. ) ;
#14929=LINE ( 'NONE', #13635, #13200 ) ;
#14938=ORIENTED_EDGE ( 'NONE', *, *, #11807, .T. ) ;
#14943=DIRECTION ( 'NONE',  ( 0.000000000000000000, -1.850371707708594316E-16, 1.000000000000000000 ) ) ;
#14948=AXIS2_PLACEMENT_3D ( 'NONE', #12203, #2865, #5097 ) ;
#14949=CARTESIAN_POINT ( 'NONE',  ( -31.79969986081099975, 20.99262100756200056, 24.21206422150099868 ) ) ;
#14952=AXIS2_PLACEMENT_3D ( 'NONE', #6175, #385, #5042 ) ;
#14954=B_SPLINE_CURVE_WITH_KNOTS ( 'NONE', 3,
 ( #1956, #11282, #732, #810 ),
 .UNSPECIFIED., .F., .F.,
 ( 4, 4 ),
 ( 0.01169941957287879905, 0.01381006638855979997 ),
 .UNSPECIFIED. ) ;
#14960=CARTESIAN_POINT ( 'NONE',  ( -18.24645429046799450, -17.08409997186676321, -13.18801804347263129 ) ) ;
#14962=ADVANCED_FACE ( 'NONE', ( #8284 ), #3782, .F. ) ;
#14980=LINE ( 'NONE', #4505, #8025 ) ;
#14983=ORIENTED_EDGE ( 'NONE', *, *, #14886, .T. ) ;
#14984=ADVANCED_FACE ( 'NONE', ( #5011, #14339 ), #9515, .T. ) ;
#14988=CARTESIAN_POINT ( 'NONE',  ( -15.49969986081099904, 9.919219809770899232, 24.21206422150099868 ) ) ;
#14991=CARTESIAN_POINT ( 'NONE',  ( -7.173558800825103887, -7.936225612681747421, 60.77745208716326886 ) ) ;
#14992=DIRECTION ( 'NONE',  ( 0.000000000000000000, 1.000000000000000000, 1.224646799147350002E-16 ) ) ;
#15002=EDGE_CURVE ( 'NONE', #1247, #4771, #945, .T. ) ;
#15009=VERTEX_POINT ( 'NONE', #12191 ) ;
#15011=B_SPLINE_CURVE_WITH_KNOTS ( 'NONE', 3,
 ( #1854, #6500, #10100, #11261, #10026, #13217, #14702, #4228, #8882, #781, #13564, #365 ),
 .UNSPECIFIED., .F., .F.,
 ( 4, 2, 2, 2, 2, 4 ),
 ( 0.000000000000000000, 0.2500000000000018874, 0.3750000000000034972, 0.4375000000000036637, 0.5000000000000037748, 1.000000000000000000 ),
 .UNSPECIFIED. ) ;
#15012=ORIENTED_EDGE ( 'NONE', *, *, #5891, .T. ) ;
#15020=EDGE_CURVE ( 'NONE', #13245, #4959, #3629, .T. ) ;
#15031=FACE_OUTER_BOUND ( 'NONE', #2424, .T. ) ;
#15032=CARTESIAN_POINT ( 'NONE',  ( -18.47295845456654106, -16.89792307448851005, -13.17045985127346341 ) ) ;
#15047=ORIENTED_EDGE ( 'NONE', *, *, #7381, .T. ) ;
#15051=DIRECTION ( 'NONE',  ( -1.767853594929135667E-17, -0.9895257890689693747, -0.1443562010009731278 ) ) ;
#15053=B_SPLINE_CURVE_WITH_KNOTS ( 'NONE', 3,
 ( #12904, #2265, #2113, #2188, #10289, #6976, #6756, #14960, #15032, #7910, #4636, #47, #11737, #7982, #13891, #1259, #11439, #12599 ),
 .UNSPECIFIED., .F., .F.,
 ( 4, 2, 2, 2, 2, 2, 2, 2, 4 ),
 ( 0.02128456778516834430, 0.02217184244320109451, 0.02305911710123384473, 0.02394639175926659494, 0.02483366641729934515, 0.02572094107533209884, 0.02660821573336484905, 0.02749549039139759926, 0.02838276504943034947 ),
 .UNSPECIFIED. ) ;
#15056=VERTEX_POINT ( 'NONE', #14560 ) ;
#15062=DIRECTION ( 'NONE',  ( 0.000000000000000000, 1.000000000000000000, 1.224646799147350002E-16 ) ) ;
#15063=AXIS2_PLACEMENT_3D ( 'NONE', #12230, #4973, #14445 ) ;
#15066=DIRECTION ( 'NONE',  ( 0.000000000000000000, 1.000000000000000000, 1.224646799147350002E-16 ) ) ;
#15074=DIRECTION ( 'NONE',  ( 1.000000000000000000, 0.000000000000000000, 0.000000000000000000 ) ) ;
#15078=DIRECTION ( 'NONE',  ( 0.000000000000000000, 2.220446049250313081E-16, -1.000000000000000000 ) ) ;
#15087=VERTEX_POINT ( 'NONE', #9891 ) ;
#15088=CARTESIAN_POINT ( 'NONE',  ( -13.50483658114444552, -17.55182216082192781, -13.23583201258599296 ) ) ;
#15090=CARTESIAN_POINT ( 'NONE',  ( -15.49969986081099371, -32.00737899243799234, -13.28793577849899599 ) ) ;
#15092=ORIENTED_EDGE ( 'NONE', *, *, #11357, .T. ) ;
#15093=DIRECTION ( 'NONE',  ( 0.000000000000000000, -1.000000000000000000, -1.224646799147350002E-16 ) ) ;
#15108=ORIENTED_EDGE ( 'NONE', *, *, #6700, .T. ) ;
ENDSEC;
END-ISO-10303-21;
